ISO-10303-21;
HEADER;
FILE_DESCRIPTION (('STEP AP214'),
    '1' );
FILE_NAME ('spur gear_am_Metric - Spur gear 2.75M 11T 20PA 23FW ---S11N75H50L18N.step',
    '2026-10-22T18:53:08',
    ( '' ),
    ( '' ),
    'SwSTEP 2.0',
    'SolidWorks 2025',
    '' );
FILE_SCHEMA (( 'AUTOMOTIVE_DESIGN' ));
ENDSEC;

DATA;
#3=ORIENTED_EDGE ( 'NONE', *, *, #12313, .F. ) ;
#9=DIRECTION ( 'NONE',  ( -1.000000000000000000, 0.000000000000000000, 0.000000000000000000 ) ) ;
#17=EDGE_CURVE ( 'NONE', #19080, #8629, #10061, .T. ) ;
#51=CARTESIAN_POINT ( 'NONE',  ( 23.00000000000000000, 10.59264252385236738, 4.936618945406631376 ) ) ;
#67=DIRECTION ( 'NONE',  ( -1.000000000000000000, -0.000000000000000000, -0.000000000000000000 ) ) ;
#85=CARTESIAN_POINT ( 'NONE',  ( 0.000000000000000000, 6.242160243097161221, 9.879763041175145588 ) ) ;
#89=DIRECTION ( 'NONE',  ( -1.000000000000000000, -0.000000000000000000, 0.000000000000000000 ) ) ;
#108=EDGE_CURVE ( 'NONE', #8629, #11642, #11625, .T. ) ;
#110=ADVANCED_FACE ( 'NONE', ( #6119 ), #2088, .T. ) ;
#134=AXIS2_PLACEMENT_3D ( 'NONE', #7164, #10463, #7038 ) ;
#135=EDGE_CURVE ( 'NONE', #23003, #4329, #4255, .T. ) ;
#152=AXIS2_PLACEMENT_3D ( 'NONE', #5788, #7824, #2121 ) ;
#157=DIRECTION ( 'NONE',  ( -1.000000000000000000, -0.000000000000000000, -0.000000000000000000 ) ) ;
#159=DIRECTION ( 'NONE',  ( -1.000000000000000000, 0.000000000000000000, 0.000000000000000000 ) ) ;
#175=CARTESIAN_POINT ( 'NONE',  ( 0.000000000000000000, -9.374578970469563899, -10.68280860024325030 ) ) ;
#180=ORIENTED_EDGE ( 'NONE', *, *, #12174, .T. ) ;
#183=EDGE_CURVE ( 'NONE', #7231, #23927, #13888, .T. ) ;
#197=ORIENTED_EDGE ( 'NONE', *, *, #13447, .T. ) ;
#229=ORIENTED_EDGE ( 'NONE', *, *, #6879, .F. ) ;
#234=DIRECTION ( 'NONE',  ( 0.000000000000000000, 0.5406408174555987767, -0.8412535328311804284 ) ) ;
#284=DIRECTION ( 'NONE',  ( -1.000000000000000000, -0.000000000000000000, 0.000000000000000000 ) ) ;
#289=CYLINDRICAL_SURFACE ( 'NONE', #1664, 17.87500000001787726 ) ;
#293=ORIENTED_EDGE ( 'NONE', *, *, #1473, .F. ) ;
#309=DIRECTION ( 'NONE',  ( -1.000000000000000000, -0.000000000000000000, 0.000000000000000000 ) ) ;
#334=CARTESIAN_POINT ( 'NONE',  ( 23.00000000000000000, -0.09016380984471503157, 11.68615217844040544 ) ) ;
#358=SHAPE_REPRESENTATION ( 'spur gear_am_Metric - Spur gear 2.75M 11T 20PA 23FW ---S11N75H50L18N', ( #8005 ), #18550 ) ;
#391=EDGE_CURVE ( 'NONE', #5706, #4329, #3496, .T. ) ;
#404=ORIENTED_EDGE ( 'NONE', *, *, #16817, .F. ) ;
#422=CARTESIAN_POINT ( 'NONE',  ( 23.00000000000000000, 11.90821470209334798, -7.758837095328730449 ) ) ;
#428=CARTESIAN_POINT ( 'NONE',  ( 23.00000000000000000, -8.772759796005177080, -7.720943453482119523 ) ) ;
#432=CARTESIAN_POINT ( 'NONE',  ( 0.000000000000000000, 0.000000000000000000, 0.000000000000000000 ) ) ;
#435=ORIENTED_EDGE ( 'NONE', *, *, #2128, .F. ) ;
#440=AXIS2_PLACEMENT_3D ( 'NONE', #7629, #21934, #9229 ) ;
#448=EDGE_CURVE ( 'NONE', #4329, #14984, #23519, .T. ) ;
#468=CIRCLE ( 'NONE', #10586, 17.87500000001787726 ) ;
#471=DIRECTION ( 'NONE',  ( -1.000000000000000000, -0.000000000000000000, -0.000000000000000000 ) ) ;
#510=CIRCLE ( 'NONE', #21501, 17.87500000001787726 ) ;
#567=CARTESIAN_POINT ( 'NONE',  ( 0.000000000000000000, -13.61176534793449200, 4.089617900950054619 ) ) ;
#576=CYLINDRICAL_SURFACE ( 'NONE', #22798, 6.050000000006051870 ) ;
#591=EDGE_CURVE ( 'NONE', #20973, #8446, #20260, .T. ) ;
#592=CIRCLE ( 'NONE', #11071, 17.87500000001787726 ) ;
#611=ORIENTED_EDGE ( 'NONE', *, *, #3056, .F. ) ;
#635=CARTESIAN_POINT ( 'NONE',  ( -10.00000000000000000, 0.000000000000000000, 0.000000000000000000 ) ) ;
#641=CYLINDRICAL_SURFACE ( 'NONE', #21938, 11.68650000001168721 ) ;
#658=CARTESIAN_POINT ( 'NONE',  ( 0.000000000000000000, 0.000000000000000000, 0.000000000000000000 ) ) ;
#698=EDGE_LOOP ( 'NONE', ( #16507, #6423, #6970, #19460 ) ) ;
#714=CARTESIAN_POINT ( 'NONE',  ( 0.000000000000000000, 0.000000000000000000, 0.000000000000000000 ) ) ;
#717=CYLINDRICAL_SURFACE ( 'NONE', #14179, 17.87500000001787726 ) ;
#719=DIRECTION ( 'NONE',  ( 0.000000000000000000, -0.9096319953545137782, -0.4154150130018965936 ) ) ;
#735=ORIENTED_EDGE ( 'NONE', *, *, #19095, .F. ) ;
#748=CARTESIAN_POINT ( 'NONE',  ( 0.000000000000000000, -15.26463740537730729, 9.300885435430041426 ) ) ;
#752=LINE ( 'NONE', #22588, #4278 ) ;
#804=DIRECTION ( 'NONE',  ( 0.000000000000000000, 0.9898214418809322401, 0.1423148382732887796 ) ) ;
#832=CYLINDRICAL_SURFACE ( 'NONE', #16173, 6.050000000006050982 ) ;
#865=CARTESIAN_POINT ( 'NONE',  ( 11.50000000000000000, -17.86986844953241516, -0.4282833139928948207 ) ) ;
#867=DIRECTION ( 'NONE',  ( -1.000000000000000000, 0.000000000000000000, 0.000000000000000000 ) ) ;
#894=EDGE_CURVE ( 'NONE', #22006, #22524, #7859, .T. ) ;
#921=EDGE_LOOP ( 'NONE', ( #1587, #18465, #20658, #20990 ) ) ;
#930=EDGE_CURVE ( 'NONE', #3367, #22006, #21537, .T. ) ;
#958=CARTESIAN_POINT ( 'NONE',  ( 0.000000000000000000, -8.772759796005278332, 7.720943453482002283 ) ) ;
#964=AXIS2_PLACEMENT_3D ( 'NONE', #3575, #16384, #23839 ) ;
#967=AXIS2_PLACEMENT_3D ( 'NONE', #15842, #14011, #1206 ) ;
#970=DIRECTION ( 'NONE',  ( -1.000000000000000000, 0.000000000000000000, 0.000000000000000000 ) ) ;
#987=CARTESIAN_POINT ( 'NONE',  ( 0.000000000000000000, -2.110835303355205639, -14.05523051341068097 ) ) ;
#989=DIRECTION ( 'NONE',  ( 0.000000000000000000, 0.000000000000000000, -1.000000000000000000 ) ) ;
#990=CARTESIAN_POINT ( 'NONE',  ( 11.49999999999999822, -15.26463740537730551, 9.300885435430041426 ) ) ;
#993=EDGE_CURVE ( 'NONE', #11156, #14408, #6731, .T. ) ;
#1005=DIRECTION ( 'NONE',  ( -1.000000000000000000, 0.000000000000000000, -0.000000000000000000 ) ) ;
#1006=AXIS2_PLACEMENT_3D ( 'NONE', #20730, #5740, #11431 ) ;
#1023=DIRECTION ( 'NONE',  ( 0.000000000000000000, 0.5406408174555986657, -0.8412535328311804284 ) ) ;
#1034=ORIENTED_EDGE ( 'NONE', *, *, #17512, .T. ) ;
#1040=VECTOR ( 'NONE', #5115, 1000.000000000000000 ) ;
#1041=DIRECTION ( 'NONE',  ( 0.000000000000000000, 0.2817325568414237313, 0.9594929736144991450 ) ) ;
#1059=CARTESIAN_POINT ( 'NONE',  ( 23.00000000000000000, 14.21257171757157955, -0.08908218613038007549 ) ) ;
#1072=CIRCLE ( 'NONE', #3389, 6.050000000006049206 ) ;
#1093=DIRECTION ( 'NONE',  ( -1.000000000000000000, 0.000000000000000000, -0.000000000000000000 ) ) ;
#1095=CARTESIAN_POINT ( 'NONE',  ( 0.000000000000000000, -6.393861490227931377, 9.782270569456429143 ) ) ;
#1100=ORIENTED_EDGE ( 'NONE', *, *, #17516, .T. ) ;
#1108=ORIENTED_EDGE ( 'NONE', *, *, #14718, .T. ) ;
#1158=LINE ( 'NONE', #5408, #4856 ) ;
#1164=AXIS2_PLACEMENT_3D ( 'NONE', #9744, #17201, #7925 ) ;
#1167=ORIENTED_EDGE ( 'NONE', *, *, #22736, .F. ) ;
#1177=CARTESIAN_POINT ( 'NONE',  ( 23.00000000000000000, 0.000000000000000000, 0.000000000000000000 ) ) ;
#1191=ORIENTED_EDGE ( 'NONE', *, *, #9608, .F. ) ;
#1203=ORIENTED_EDGE ( 'NONE', *, *, #9730, .F. ) ;
#1206=DIRECTION ( 'NONE',  ( 0.000000000000000000, 0.000000000000000000, 1.000000000000000000 ) ) ;
#1218=CIRCLE ( 'NONE', #14436, 17.87500000001787726 ) ;
#1221=DIRECTION ( 'NONE',  ( -1.000000000000000000, 0.000000000000000000, 0.000000000000000000 ) ) ;
#1228=LINE ( 'NONE', #990, #5175 ) ;
#1246=VERTEX_POINT ( 'NONE', #12664 ) ;
#1252=DIRECTION ( 'NONE',  ( -1.000000000000000000, 0.000000000000000000, -0.000000000000000000 ) ) ;
#1277=VECTOR ( 'NONE', #2666, 1000.000000000000000 ) ;
#1278=ORIENTED_EDGE ( 'NONE', *, *, #108, .T. ) ;
#1314=DIRECTION ( 'NONE',  ( 0.000000000000000000, 0.000000000000000000, 1.000000000000000000 ) ) ;
#1327=AXIS2_PLACEMENT_3D ( 'NONE', #19592, #10160, #2869 ) ;
#1337=CARTESIAN_POINT ( 'NONE',  ( 23.00000000000000000, -7.812991839788663739, -16.07708877602020792 ) ) ;
#1347=VERTEX_POINT ( 'NONE', #11889 ) ;
#1349=DIRECTION ( 'NONE',  ( -1.000000000000000000, -0.000000000000000000, 0.000000000000000000 ) ) ;
#1355=AXIS2_PLACEMENT_3D ( 'NONE', #3508, #12518, #19991 ) ;
#1366=VECTOR ( 'NONE', #20697, 1000.000000000000000 ) ;
#1379=CARTESIAN_POINT ( 'NONE',  ( 23.00000000000000000, -2.110835303355205639, -14.05523051341068097 ) ) ;
#1394=CARTESIAN_POINT ( 'NONE',  ( 0.000000000000000000, 8.890849273385706297, -7.584660931657394300 ) ) ;
#1420=ORIENTED_EDGE ( 'NONE', *, *, #14208, .T. ) ;
#1460=ORIENTED_EDGE ( 'NONE', *, *, #108, .F. ) ;
#1466=ORIENTED_EDGE ( 'NONE', *, *, #15552, .F. ) ;
#1468=DIRECTION ( 'NONE',  ( -1.000000000000000000, -0.000000000000000000, 0.000000000000000000 ) ) ;
#1473=EDGE_CURVE ( 'NONE', #16008, #4837, #510, .T. ) ;
#1514=ORIENTED_EDGE ( 'NONE', *, *, #17, .F. ) ;
#1531=VERTEX_POINT ( 'NONE', #16611 ) ;
#1547=CARTESIAN_POINT ( 'NONE',  ( 0.000000000000000000, 0.000000000000000000, 0.000000000000000000 ) ) ;
#1563=DIRECTION ( 'NONE',  ( -1.000000000000000000, 0.000000000000000000, 0.000000000000000000 ) ) ;
#1564=DIRECTION ( 'NONE',  ( -1.000000000000000000, -0.000000000000000000, -0.000000000000000000 ) ) ;
#1566=CYLINDRICAL_SURFACE ( 'NONE', #1355, 6.050000000006051870 ) ;
#1578=CARTESIAN_POINT ( 'NONE',  ( 23.00000000000000000, 0.000000000000000000, 0.000000000000000000 ) ) ;
#1587=ORIENTED_EDGE ( 'NONE', *, *, #14769, .F. ) ;
#1591=DIRECTION ( 'NONE',  ( 0.000000000000000000, 0.000000000000000000, 1.000000000000000000 ) ) ;
#1611=ORIENTED_EDGE ( 'NONE', *, *, #10765, .F. ) ;
#1618=DIRECTION ( 'NONE',  ( 0.000000000000000000, 0.2817325568414236758, 0.9594929736144991450 ) ) ;
#1626=AXIS2_PLACEMENT_3D ( 'NONE', #11724, #6023, #13210 ) ;
#1645=DIRECTION ( 'NONE',  ( 0.000000000000000000, 0.000000000000000000, 1.000000000000000000 ) ) ;
#1650=CARTESIAN_POINT ( 'NONE',  ( 23.00000000000000000, -3.205857990849673378, -11.23818298448545860 ) ) ;
#1664=AXIS2_PLACEMENT_3D ( 'NONE', #9285, #20289, #7569 ) ;
#1688=CARTESIAN_POINT ( 'NONE',  ( 23.00000000000000000, 0.000000000000000000, 0.000000000000000000 ) ) ;
#1699=DIRECTION ( 'NONE',  ( 0.000000000000000000, 0.000000000000000000, 1.000000000000000000 ) ) ;
#1740=ORIENTED_EDGE ( 'NONE', *, *, #2156, .T. ) ;
#1756=VERTEX_POINT ( 'NONE', #1768 ) ;
#1768=CARTESIAN_POINT ( 'NONE',  ( 0.000000000000000000, -10.66755332433025316, 4.772587172891003426 ) ) ;
#1781=ORIENTED_EDGE ( 'NONE', *, *, #14603, .F. ) ;
#1794=LINE ( 'NONE', #20329, #7612 ) ;
#1797=ORIENTED_EDGE ( 'NONE', *, *, #9368, .T. ) ;
#1809=DIRECTION ( 'NONE',  ( 0.000000000000000000, 0.2817325568414237313, 0.9594929736144991450 ) ) ;
#1824=DIRECTION ( 'NONE',  ( -1.000000000000000000, 0.000000000000000000, 0.000000000000000000 ) ) ;
#1829=CIRCLE ( 'NONE', #2610, 6.050000000006051870 ) ;
#1859=EDGE_CURVE ( 'NONE', #22027, #14408, #8326, .T. ) ;
#1867=CARTESIAN_POINT ( 'NONE',  ( 23.00000000000000000, -9.239931321968100519, -10.79948145182508057 ) ) ;
#1896=ORIENTED_EDGE ( 'NONE', *, *, #13667, .T. ) ;
#1899=SHAPE_DEFINITION_REPRESENTATION ( #11302, #358 ) ;
#1900=ORIENTED_EDGE ( 'NONE', *, *, #2767, .T. ) ;
#1901=ORIENTED_EDGE ( 'NONE', *, *, #6858, .F. ) ;
#1905=DIRECTION ( 'NONE',  ( -1.000000000000000000, 0.000000000000000000, 0.000000000000000000 ) ) ;
#1927=FACE_OUTER_BOUND ( 'NONE', #6392, .T. ) ;
#1928=CYLINDRICAL_SURFACE ( 'NONE', #6866, 17.87500000001787726 ) ;
#1946=DIRECTION ( 'NONE',  ( -1.000000000000000000, 0.000000000000000000, 0.000000000000000000 ) ) ;
#1953=DIRECTION ( 'NONE',  ( 0.000000000000000000, 0.000000000000000000, 1.000000000000000000 ) ) ;
#1968=DIRECTION ( 'NONE',  ( 0.000000000000000000, 0.000000000000000000, 1.000000000000000000 ) ) ;
#1972=ORIENTED_EDGE ( 'NONE', *, *, #9730, .T. ) ;
#2002=CIRCLE ( 'NONE', #10183, 17.87500000001787726 ) ;
#2011=CARTESIAN_POINT ( 'NONE',  ( 0.000000000000000000, 17.26667456984545979, 4.623588898214379128 ) ) ;
#2020=ORIENTED_EDGE ( 'NONE', *, *, #10962, .T. ) ;
#2023=CARTESIAN_POINT ( 'NONE',  ( 23.00000000000000000, -7.033831428820075615, -16.43291941292179459 ) ) ;
#2087=AXIS2_PLACEMENT_3D ( 'NONE', #5542, #22622, #4087 ) ;
#2088=CYLINDRICAL_SURFACE ( 'NONE', #23377, 11.68650000001168721 ) ;
#2090=CIRCLE ( 'NONE', #13008, 11.68650000001168543 ) ;
#2098=DIRECTION ( 'NONE',  ( -1.000000000000000000, 0.000000000000000000, -0.000000000000000000 ) ) ;
#2121=DIRECTION ( 'NONE',  ( 0.000000000000000000, 0.000000000000000000, -1.000000000000000000 ) ) ;
#2128=EDGE_CURVE ( 'NONE', #6155, #8876, #17062, .T. ) ;
#2134=CIRCLE ( 'NONE', #23189, 6.050000000006054535 ) ;
#2137=ORIENTED_EDGE ( 'NONE', *, *, #2679, .F. ) ;
#2142=ORIENTED_EDGE ( 'NONE', *, *, #8463, .F. ) ;
#2149=DIRECTION ( 'NONE',  ( 0.000000000000000000, 0.000000000000000000, 1.000000000000000000 ) ) ;
#2156=EDGE_CURVE ( 'NONE', #5794, #20283, #21385, .T. ) ;
#2173=VECTOR ( 'NONE', #8482, 1000.000000000000000 ) ;
#2177=DIRECTION ( 'NONE',  ( 0.000000000000000000, 0.000000000000000000, 1.000000000000000000 ) ) ;
#2192=AXIS2_PLACEMENT_3D ( 'NONE', #8280, #15732, #23197 ) ;
#2203=CIRCLE ( 'NONE', #7252, 11.68650000001168898 ) ;
#2214=DIRECTION ( 'NONE',  ( 0.000000000000000000, -0.5406408174555871193, -0.8412535328311879779 ) ) ;
#2236=CARTESIAN_POINT ( 'NONE',  ( 23.00000000000000000, 11.90821470209334798, -7.758837095328730449 ) ) ;
#2247=CARTESIAN_POINT ( 'NONE',  ( 23.00000000000000000, -13.61176534793449200, 4.089617900950054619 ) ) ;
#2248=CARTESIAN_POINT ( 'NONE',  ( 23.00000000000000000, 6.242160243097294448, -9.879763041175060323 ) ) ;
#2276=DIRECTION ( 'NONE',  ( -1.000000000000000000, -0.000000000000000000, -0.000000000000000000 ) ) ;
#2288=ORIENTED_EDGE ( 'NONE', *, *, #11297, .T. ) ;
#2292=FACE_OUTER_BOUND ( 'NONE', #10702, .T. ) ;
#2304=CARTESIAN_POINT ( 'NONE',  ( 11.49999999999999822, 11.37860023611340665, 13.78561139983856521 ) ) ;
#2305=DIRECTION ( 'NONE',  ( 0.000000000000000000, 0.000000000000000000, 1.000000000000000000 ) ) ;
#2333=DIRECTION ( 'NONE',  ( -1.000000000000000000, 0.000000000000000000, 0.000000000000000000 ) ) ;
#2336=VERTEX_POINT ( 'NONE', #20258 ) ;
#2339=CARTESIAN_POINT ( 'NONE',  ( 23.00000000000000000, -17.86986844953242937, 0.4282833139926502386 ) ) ;
#2356=CARTESIAN_POINT ( 'NONE',  ( 23.00000000000000000, -3.205857990849673378, -11.23818298448545860 ) ) ;
#2371=ORIENTED_EDGE ( 'NONE', *, *, #21131, .T. ) ;
#2385=DIRECTION ( 'NONE',  ( -1.000000000000000000, -0.000000000000000000, 0.000000000000000000 ) ) ;
#2432=MANIFOLD_SOLID_BREP ( 'Bore', #5036 ) ;
#2480=DIRECTION ( 'NONE',  ( 0.000000000000000000, 0.000000000000000000, 1.000000000000000000 ) ) ;
#2489=EDGE_LOOP ( 'NONE', ( #13194, #2536 ) ) ;
#2522=CIRCLE ( 'NONE', #4877, 6.050000000006050982 ) ;
#2525=ADVANCED_FACE ( 'NONE', ( #11533 ), #19004, .T. ) ;
#2536=ORIENTED_EDGE ( 'NONE', *, *, #21931, .F. ) ;
#2537=CARTESIAN_POINT ( 'NONE',  ( 23.00000000000000000, 0.000000000000000000, 0.000000000000000000 ) ) ;
#2554=DIRECTION ( 'NONE',  ( 0.000000000000000000, 0.000000000000000000, 1.000000000000000000 ) ) ;
#2569=CARTESIAN_POINT ( 'NONE',  ( 0.000000000000000000, -11.55437235128774809, 1.752358929577604085 ) ) ;
#2572=CYLINDRICAL_SURFACE ( 'NONE', #17215, 11.68650000001168721 ) ;
#2573=EDGE_CURVE ( 'NONE', #11737, #12175, #13132, .T. ) ;
#2589=DIRECTION ( 'NONE',  ( 0.000000000000000000, 0.000000000000000000, 1.000000000000000000 ) ) ;
#2602=ORIENTED_EDGE ( 'NONE', *, *, #18125, .T. ) ;
#2610=AXIS2_PLACEMENT_3D ( 'NONE', #1867, #18815, #20770 ) ;
#2615=CARTESIAN_POINT ( 'NONE',  ( 23.00000000000000000, 8.890849273385706297, -7.584660931657394300 ) ) ;
#2626=ORIENTED_EDGE ( 'NONE', *, *, #18380, .T. ) ;
#2657=DIRECTION ( 'NONE',  ( 0.000000000000000000, -0.7557495743542635980, 0.6548607339452787723 ) ) ;
#2666=DIRECTION ( 'NONE',  ( -1.000000000000000000, 0.000000000000000000, 0.000000000000000000 ) ) ;
#2670=FACE_OUTER_BOUND ( 'NONE', #7422, .T. ) ;
#2679=EDGE_CURVE ( 'NONE', #18077, #4837, #8764, .T. ) ;
#2687=FACE_OUTER_BOUND ( 'NONE', #7204, .T. ) ;
#2699=LINE ( 'NONE', #19676, #17937 ) ;
#2715=ORIENTED_EDGE ( 'NONE', *, *, #7071, .T. ) ;
#2720=ORIENTED_EDGE ( 'NONE', *, *, #19934, .F. ) ;
#2728=CARTESIAN_POINT ( 'NONE',  ( 23.00000000000000000, 8.890849273385706297, -7.584660931657394300 ) ) ;
#2737=ORIENTED_EDGE ( 'NONE', *, *, #8581, .T. ) ;
#2741=VERTEX_POINT ( 'NONE', #11341 ) ;
#2752=CYLINDRICAL_SURFACE ( 'NONE', #6471, 11.68650000001168721 ) ;
#2767=EDGE_CURVE ( 'NONE', #4844, #10574, #23590, .T. ) ;
#2768=ADVANCED_FACE ( 'NONE', ( #2687 ), #10103, .F. ) ;
#2810=CARTESIAN_POINT ( 'NONE',  ( 23.00000000000000000, 2.119223430970166522, 17.74893002550480503 ) ) ;
#2812=DIRECTION ( 'NONE',  ( 0.000000000000000000, 0.000000000000000000, -1.000000000000000000 ) ) ;
#2824=CARTESIAN_POINT ( 'NONE',  ( 23.00000000000000000, 11.90821470209324140, 7.758837095328885880 ) ) ;
#2831=DIRECTION ( 'NONE',  ( -1.000000000000000000, 0.000000000000000000, -0.000000000000000000 ) ) ;
#2835=CARTESIAN_POINT ( 'NONE',  ( 23.00000000000000000, 11.58003564732003277, 1.573866785045813899 ) ) ;
#2838=ADVANCED_FACE ( 'NONE', ( #23785 ), #3061, .T. ) ;
#2847=DIRECTION ( 'NONE',  ( -1.000000000000000000, -0.000000000000000000, 0.000000000000000000 ) ) ;
#2849=DIRECTION ( 'NONE',  ( 0.000000000000000000, 0.000000000000000000, 1.000000000000000000 ) ) ;
#2869=DIRECTION ( 'NONE',  ( 0.000000000000000000, -0.7557495743542638200, 0.6548607339452786613 ) ) ;
#2888=CIRCLE ( 'NONE', #16511, 11.68650000001168543 ) ;
#2892=CARTESIAN_POINT ( 'NONE',  ( 0.000000000000000000, 0.000000000000000000, 0.000000000000000000 ) ) ;
#2922=EDGE_LOOP ( 'NONE', ( #3108, #17399 ) ) ;
#2954=ORIENTED_EDGE ( 'NONE', *, *, #11297, .F. ) ;
#2958=CARTESIAN_POINT ( 'NONE',  ( 23.00000000000000000, -14.80154252341802312, 10.02147513732818851 ) ) ;
#2982=PLANE ( 'NONE',  #8260 ) ;
#3004=CYLINDRICAL_SURFACE ( 'NONE', #18872, 6.050000000006050982 ) ;
#3052=ORIENTED_EDGE ( 'NONE', *, *, #16126, .F. ) ;
#3056=EDGE_CURVE ( 'NONE', #20166, #23530, #16554, .T. ) ;
#3061=CYLINDRICAL_SURFACE ( 'NONE', #15024, 6.050000000006051870 ) ;
#3075=CYLINDRICAL_SURFACE ( 'NONE', #12164, 6.050000000006052758 ) ;
#3087=ORIENTED_EDGE ( 'NONE', *, *, #16336, .T. ) ;
#3093=EDGE_CURVE ( 'NONE', #12041, #15398, #18521, .T. ) ;
#3108=ORIENTED_EDGE ( 'NONE', *, *, #20780, .F. ) ;
#3131=DIRECTION ( 'NONE',  ( 1.000000000000000000, -0.000000000000000000, -0.000000000000000000 ) ) ;
#3136=DIRECTION ( 'NONE',  ( -1.000000000000000000, -0.000000000000000000, -0.000000000000000000 ) ) ;
#3169=FACE_OUTER_BOUND ( 'NONE', #6961, .T. ) ;
#3191=EDGE_CURVE ( 'NONE', #15261, #4544, #5665, .T. ) ;
#3194=ORIENTED_EDGE ( 'NONE', *, *, #19959, .T. ) ;
#3199=VECTOR ( 'NONE', #10693, 1000.000000000000000 ) ;
#3205=ADVANCED_FACE ( 'NONE', ( #23413 ), #6688, .T. ) ;
#3224=CARTESIAN_POINT ( 'NONE',  ( 23.00000000000000000, 6.242160243097161221, 9.879763041175145588 ) ) ;
#3225=VERTEX_POINT ( 'NONE', #4990 ) ;
#3262=CARTESIAN_POINT ( 'NONE',  ( 23.00000000000000000, 0.000000000000000000, 0.000000000000000000 ) ) ;
#3263=CIRCLE ( 'NONE', #6324, 17.87500000001787726 ) ;
#3270=AXIS2_PLACEMENT_3D ( 'NONE', #20453, #3382, #3741 ) ;
#3272=( NAMED_UNIT ( * ) SI_UNIT ( $, .STERADIAN. ) SOLID_ANGLE_UNIT ( ) );
#3276=ORIENTED_EDGE ( 'NONE', *, *, #2128, .T. ) ;
#3282=SHAPE_REPRESENTATION_RELATIONSHIP ( 'NONE' , 'NONE' ,  #358, #11311 ) ;
#3285=FACE_OUTER_BOUND ( 'NONE', #13998, .T. ) ;
#3346=AXIS2_PLACEMENT_3D ( 'NONE', #10896, #67, #13106 ) ;
#3347=ORIENTED_EDGE ( 'NONE', *, *, #6348, .T. ) ;
#3367=VERTEX_POINT ( 'NONE', #1394 ) ;
#3374=DIRECTION ( 'NONE',  ( -1.000000000000000000, -0.000000000000000000, -0.000000000000000000 ) ) ;
#3382=DIRECTION ( 'NONE',  ( -1.000000000000000000, 0.000000000000000000, 0.000000000000000000 ) ) ;
#3384=DIRECTION ( 'NONE',  ( 0.000000000000000000, 0.000000000000000000, -1.000000000000000000 ) ) ;
#3389=AXIS2_PLACEMENT_3D ( 'NONE', #1379, #9019, #16468 ) ;
#3390=LINE ( 'NONE', #12879, #16440 ) ;
#3393=CYLINDRICAL_SURFACE ( 'NONE', #4771, 17.87500000001787726 ) ;
#3428=ORIENTED_EDGE ( 'NONE', *, *, #3668, .F. ) ;
#3443=CARTESIAN_POINT ( 'NONE',  ( 0.000000000000000000, 11.58003564732003277, 1.573866785045813899 ) ) ;
#3455=CARTESIAN_POINT ( 'NONE',  ( 0.000000000000000000, -17.86986844953242937, 0.4282833139926494059 ) ) ;
#3496=CIRCLE ( 'NONE', #6626, 17.87500000001787726 ) ;
#3503=CARTESIAN_POINT ( 'NONE',  ( 50.00005079999999680, 0.000000000000000000, 9.000000000000000000 ) ) ;
#3508=CARTESIAN_POINT ( 'NONE',  ( 23.00000000000000000, 5.985147671565880678, -12.89120389306408754 ) ) ;
#3520=ORIENTED_EDGE ( 'NONE', *, *, #22146, .T. ) ;
#3523=CARTESIAN_POINT ( 'NONE',  ( 23.00000000000000000, 0.000000000000000000, 0.000000000000000000 ) ) ;
#3524=CARTESIAN_POINT ( 'NONE',  ( 23.00000000000000000, 0.000000000000000000, 0.000000000000000000 ) ) ;
#3575=CARTESIAN_POINT ( 'NONE',  ( 0.000000000000000000, -9.239931321968100519, -10.79948145182508057 ) ) ;
#3590=CARTESIAN_POINT ( 'NONE',  ( 23.00000000000000000, -13.66196005206966468, 3.918670437617043145 ) ) ;
#3611=ADVANCED_FACE ( 'NONE', ( #13124 ), #20690, .T. ) ;
#3616=ORIENTED_EDGE ( 'NONE', *, *, #5515, .T. ) ;
#3617=VECTOR ( 'NONE', #89, 1000.000000000000000 ) ;
#3623=( LENGTH_UNIT ( ) NAMED_UNIT ( * ) SI_UNIT ( .MILLI., .METRE. ) );
#3654=DIRECTION ( 'NONE',  ( -1.000000000000000000, -0.000000000000000000, -0.000000000000000000 ) ) ;
#3656=CYLINDRICAL_SURFACE ( 'NONE', #11657, 6.050000000006050982 ) ;
#3668=EDGE_CURVE ( 'NONE', #4544, #11156, #20980, .T. ) ;
#3712=VERTEX_POINT ( 'NONE', #14942 ) ;
#3741=DIRECTION ( 'NONE',  ( 0.000000000000000000, 0.000000000000000000, 1.000000000000000000 ) ) ;
#3744=FACE_OUTER_BOUND ( 'NONE', #18619, .T. ) ;
#3791=EDGE_CURVE ( 'NONE', #15261, #4197, #6546, .T. ) ;
#3817=CARTESIAN_POINT ( 'NONE',  ( 23.00000000000000000, 12.00453763395397466, 7.608955687739546114 ) ) ;
#3819=EDGE_LOOP ( 'NONE', ( #1203, #1901, #14356, #15271 ) ) ;
#3827=FACE_OUTER_BOUND ( 'NONE', #21662, .T. ) ;
#3834=DIRECTION ( 'NONE',  ( -1.000000000000000000, -0.000000000000000000, -0.000000000000000000 ) ) ;
#3842=LINE ( 'NONE', #1650, #22845 ) ;
#3849=ORIENTED_EDGE ( 'NONE', *, *, #6533, .F. ) ;
#3866=DIRECTION ( 'NONE',  ( 0.000000000000000000, 0.000000000000000000, 1.000000000000000000 ) ) ;
#3885=DIRECTION ( 'NONE',  ( -1.000000000000000000, -0.000000000000000000, -0.000000000000000000 ) ) ;
#3900=AXIS2_PLACEMENT_3D ( 'NONE', #4915, #12329, #19797 ) ;
#3911=VECTOR ( 'NONE', #21380, 1000.000000000000000 ) ;
#3920=DIRECTION ( 'NONE',  ( -1.000000000000000000, 0.000000000000000000, -0.000000000000000000 ) ) ;
#3925=LINE ( 'NONE', #11108, #23863 ) ;
#3958=EDGE_LOOP ( 'NONE', ( #19542, #1797, #15613, #17708 ) ) ;
#3966=CIRCLE ( 'NONE', #1626, 17.87500000001787726 ) ;
#3973=EDGE_CURVE ( 'NONE', #8446, #6823, #6115, .T. ) ;
#3976=FACE_OUTER_BOUND ( 'NONE', #6159, .T. ) ;
#4009=CARTESIAN_POINT ( 'NONE',  ( 11.50000000000000000, -7.033831428820063181, -16.43291941292179104 ) ) ;
#4010=CARTESIAN_POINT ( 'NONE',  ( 23.00000000000000000, 0.000000000000000000, 0.000000000000000000 ) ) ;
#4018=CARTESIAN_POINT ( 'NONE',  ( 23.00000000000000000, -3.205857990849823480, 11.23818298448541420 ) ) ;
#4020=AXIS2_PLACEMENT_3D ( 'NONE', #7743, #20692, #2149 ) ;
#4037=LINE ( 'NONE', #13552, #22689 ) ;
#4044=CARTESIAN_POINT ( 'NONE',  ( 23.00000000000000000, 5.985147671565880678, -12.89120389306408754 ) ) ;
#4079=EDGE_LOOP ( 'NONE', ( #13477, #3520, #1781, #293 ) ) ;
#4084=VECTOR ( 'NONE', #9617, 1000.000000000000000 ) ;
#4087=DIRECTION ( 'NONE',  ( 0.000000000000000000, -0.5406408174555868973, -0.8412535328311879779 ) ) ;
#4123=ORIENTED_EDGE ( 'NONE', *, *, #183, .T. ) ;
#4130=AXIS2_PLACEMENT_3D ( 'NONE', #9706, #9465, #234 ) ;
#4143=DIRECTION ( 'NONE',  ( 0.000000000000000000, 0.000000000000000000, 1.000000000000000000 ) ) ;
#4153=ORIENTED_EDGE ( 'NONE', *, *, #23419, .F. ) ;
#4170=FACE_OUTER_BOUND ( 'NONE', #4572, .T. ) ;
#4177=DIRECTION ( 'NONE',  ( 0.000000000000000000, 0.000000000000000000, 1.000000000000000000 ) ) ;
#4181=ADVANCED_FACE ( 'NONE', ( #3827 ), #11236, .T. ) ;
#4197=VERTEX_POINT ( 'NONE', #13692 ) ;
#4205=DIRECTION ( 'NONE',  ( 0.000000000000000000, 0.000000000000000000, 1.000000000000000000 ) ) ;
#4227=DIRECTION ( 'NONE',  ( -1.000000000000000000, 0.000000000000000000, 0.000000000000000000 ) ) ;
#4255=CIRCLE ( 'NONE', #1164, 6.050000000006050982 ) ;
#4268=LINE ( 'NONE', #19140, #16912 ) ;
#4276=DIRECTION ( 'NONE',  ( 0.000000000000000000, 0.000000000000000000, 1.000000000000000000 ) ) ;
#4278=VECTOR ( 'NONE', #7924, 1000.000000000000000 ) ;
#4294=VECTOR ( 'NONE', #867, 1000.000000000000000 ) ;
#4329=VERTEX_POINT ( 'NONE', #2011 ) ;
#4346=DIRECTION ( 'NONE',  ( 0.000000000000000000, 0.000000000000000000, 1.000000000000000000 ) ) ;
#4378=EDGE_LOOP ( 'NONE', ( #20286, #5573, #7676, #8909 ) ) ;
#4380=DIRECTION ( 'NONE',  ( -1.000000000000000000, 0.000000000000000000, 0.000000000000000000 ) ) ;
#4382=CARTESIAN_POINT ( 'NONE',  ( 23.00000000000000000, -9.374578970469700678, 10.68280860024311885 ) ) ;
#4405=CIRCLE ( 'NONE', #23498, 6.050000000006054535 ) ;
#4418=DIRECTION ( 'NONE',  ( -1.000000000000000000, 0.000000000000000000, 0.000000000000000000 ) ) ;
#4419=CIRCLE ( 'NONE', #7478, 6.050000000006050982 ) ;
#4431=EDGE_CURVE ( 'NONE', #4471, #7020, #14177, .T. ) ;
#4453=CARTESIAN_POINT ( 'NONE',  ( 23.00000000000000000, 0.000000000000000000, 0.000000000000000000 ) ) ;
#4471=VERTEX_POINT ( 'NONE', #21305 ) ;
#4538=CARTESIAN_POINT ( 'NONE',  ( 23.00000000000000000, 14.21257171757157245, 0.08908218613057176938 ) ) ;
#4544=VERTEX_POINT ( 'NONE', #13604 ) ;
#4558=CARTESIAN_POINT ( 'NONE',  ( 23.00000000000000000, 12.00453763395396756, -1.558955687733494244 ) ) ;
#4561=DIRECTION ( 'NONE',  ( 0.000000000000000000, 0.000000000000000000, 1.000000000000000000 ) ) ;
#4566=EDGE_LOOP ( 'NONE', ( #4760, #17620, #21464, #12169 ) ) ;
#4572=EDGE_LOOP ( 'NONE', ( #5341, #20187, #19424, #21220 ) ) ;
#4585=ORIENTED_EDGE ( 'NONE', *, *, #9149, .T. ) ;
#4597=CARTESIAN_POINT ( 'NONE',  ( 0.000000000000000000, 6.242160243097294448, -9.879763041175060323 ) ) ;
#4601=CARTESIAN_POINT ( 'NONE',  ( 23.00000000000000000, 5.985147671565707483, 12.89120389306417103 ) ) ;
#4613=DIRECTION ( 'NONE',  ( 0.000000000000000000, 0.000000000000000000, 1.000000000000000000 ) ) ;
#4615=ORIENTED_EDGE ( 'NONE', *, *, #7071, .F. ) ;
#4629=ORIENTED_EDGE ( 'NONE', *, *, #6491, .T. ) ;
#4633=DIRECTION ( 'NONE',  ( -1.000000000000000000, -0.000000000000000000, -0.000000000000000000 ) ) ;
#4635=EDGE_CURVE ( 'NONE', #15398, #19205, #8318, .T. ) ;
#4637=CARTESIAN_POINT ( 'NONE',  ( 0.000000000000000000, -11.55437235128772500, -1.752358929577761515 ) ) ;
#4643=ORIENTED_EDGE ( 'NONE', *, *, #14603, .T. ) ;
#4660=DIRECTION ( 'NONE',  ( -1.000000000000000000, -0.000000000000000000, -0.000000000000000000 ) ) ;
#4663=FACE_OUTER_BOUND ( 'NONE', #23790, .T. ) ;
#4717=CARTESIAN_POINT ( 'NONE',  ( 0.000000000000000000, -0.09016380984455869829, -11.68615217844040721 ) ) ;
#4750=DIRECTION ( 'NONE',  ( 0.000000000000000000, 0.9096319953545193293, -0.4154150130018841591 ) ) ;
#4759=CIRCLE ( 'NONE', #16412, 6.050000000006050982 ) ;
#4760=ORIENTED_EDGE ( 'NONE', *, *, #22229, .F. ) ;
#4771=AXIS2_PLACEMENT_3D ( 'NONE', #12297, #1564, #16421 ) ;
#4776=VERTEX_POINT ( 'NONE', #20163 ) ;
#4835=VECTOR ( 'NONE', #5581, 1000.000000000000000 ) ;
#4837=VERTEX_POINT ( 'NONE', #18922 ) ;
#4844=VERTEX_POINT ( 'NONE', #10956 ) ;
#4856=VECTOR ( 'NONE', #16499, 1000.000000000000000 ) ;
#4866=ORIENTED_EDGE ( 'NONE', *, *, #6503, .F. ) ;
#4867=CARTESIAN_POINT ( 'NONE',  ( 0.000000000000000000, 17.26667456984545268, -4.623588898214372911 ) ) ;
#4876=ADVANCED_FACE ( 'NONE', ( #5625 ), #13050, .T. ) ;
#4877=AXIS2_PLACEMENT_3D ( 'NONE', #14940, #5451, #9222 ) ;
#4910=CIRCLE ( 'NONE', #18533, 11.68650000001168721 ) ;
#4915=CARTESIAN_POINT ( 'NONE',  ( 0.000000000000000000, 11.90821470209334798, -7.758837095328730449 ) ) ;
#4961=ORIENTED_EDGE ( 'NONE', *, *, #8172, .F. ) ;
#4968=DIRECTION ( 'NONE',  ( -1.000000000000000000, 0.000000000000000000, -0.000000000000000000 ) ) ;
#4980=ORIENTED_EDGE ( 'NONE', *, *, #7590, .T. ) ;
#4984=ORIENTED_EDGE ( 'NONE', *, *, #4431, .T. ) ;
#4990=CARTESIAN_POINT ( 'NONE',  ( 23.00000000000000000, -6.393861490227931377, 9.782270569456429143 ) ) ;
#4992=ADVANCED_FACE ( 'NONE', ( #23188 ), #17552, .T. ) ;
#4995=CYLINDRICAL_SURFACE ( 'NONE', #967, 6.050000000006051870 ) ;
#5021=EDGE_CURVE ( 'NONE', #23953, #11737, #20046, .T. ) ;
#5036=CLOSED_SHELL ( 'NONE', ( #13881, #16282, #16849, #10644, #19462, #6342, #2525, #8672, #7591, #10012, #12466, #21170, #22092, #16089, #19678, #10253, #10115, #12375, #17953, #23814, #110, #8776, #20949, #4876, #21471, #14510, #9542, #3611, #7948, #13480, #15856, #3205, #18271, #20591, #16503, #14327, #20663, #4181, #14607, #7650, #11968, #11469, #4992, #17095, #21837, #8541, #20050, #14896, #2838, #17523, #6658, #2768 ) ) ;
#5052=DIRECTION ( 'NONE',  ( -1.000000000000000000, -0.000000000000000000, -0.000000000000000000 ) ) ;
#5076=CARTESIAN_POINT ( 'NONE',  ( 23.00000000000000000, 0.000000000000000000, 0.000000000000000000 ) ) ;
#5093=CARTESIAN_POINT ( 'NONE',  ( 0.000000000000000000, 10.59264252385243665, -4.936618945406485714 ) ) ;
#5115=DIRECTION ( 'NONE',  ( 1.000000000000000000, -0.000000000000000000, -0.000000000000000000 ) ) ;
#5130=ORIENTED_EDGE ( 'NONE', *, *, #22164, .T. ) ;
#5175=VECTOR ( 'NONE', #14268, 1000.000000000000000 ) ;
#5176=CIRCLE ( 'NONE', #15283, 11.68650000001168543 ) ;
#5179=ORIENTED_EDGE ( 'NONE', *, *, #22529, .T. ) ;
#5186=CYLINDRICAL_SURFACE ( 'NONE', #18158, 6.050000000006050982 ) ;
#5220=CIRCLE ( 'NONE', #7525, 6.050000000006051870 ) ;
#5226=ORIENTED_EDGE ( 'NONE', *, *, #894, .T. ) ;
#5260=ORIENTED_EDGE ( 'NONE', *, *, #16902, .T. ) ;
#5269=DIRECTION ( 'NONE',  ( -1.000000000000000000, -0.000000000000000000, -0.000000000000000000 ) ) ;
#5310=CIRCLE ( 'NONE', #21281, 6.050000000006052758 ) ;
#5311=EDGE_CURVE ( 'NONE', #23953, #10776, #17064, .T. ) ;
#5341=ORIENTED_EDGE ( 'NONE', *, *, #22832, .F. ) ;
#5362=CYLINDRICAL_SURFACE ( 'NONE', #20071, 11.68650000001168721 ) ;
#5404=DIRECTION ( 'NONE',  ( -1.000000000000000000, 0.000000000000000000, -0.000000000000000000 ) ) ;
#5408=CARTESIAN_POINT ( 'NONE',  ( 11.50000000000000000, -7.812991839788874238, 16.07708877602009068 ) ) ;
#5451=DIRECTION ( 'NONE',  ( 1.000000000000000000, 0.000000000000000000, 0.000000000000000000 ) ) ;
#5457=VECTOR ( 'NONE', #18307, 1000.000000000000000 ) ;
#5464=FACE_OUTER_BOUND ( 'NONE', #10215, .T. ) ;
#5515=EDGE_CURVE ( 'NONE', #14903, #9833, #19292, .T. ) ;
#5525=DIRECTION ( 'NONE',  ( 1.000000000000000000, 0.000000000000000000, 0.000000000000000000 ) ) ;
#5542=CARTESIAN_POINT ( 'NONE',  ( 0.000000000000000000, 0.000000000000000000, 0.000000000000000000 ) ) ;
#5573=ORIENTED_EDGE ( 'NONE', *, *, #3973, .F. ) ;
#5581=DIRECTION ( 'NONE',  ( -1.000000000000000000, 0.000000000000000000, 0.000000000000000000 ) ) ;
#5583=DIRECTION ( 'NONE',  ( 0.000000000000000000, 0.000000000000000000, 1.000000000000000000 ) ) ;
#5588=ORIENTED_EDGE ( 'NONE', *, *, #21931, .T. ) ;
#5592=AXIS2_PLACEMENT_3D ( 'NONE', #4382, #19271, #2554 ) ;
#5594=DIRECTION ( 'NONE',  ( -1.000000000000000000, -0.000000000000000000, -0.000000000000000000 ) ) ;
#5595=AXIS2_PLACEMENT_3D ( 'NONE', #11727, #3834, #20921 ) ;
#5600=CARTESIAN_POINT ( 'NONE',  ( 23.00000000000000000, -9.239931321968100519, -10.79948145182508057 ) ) ;
#5625=FACE_OUTER_BOUND ( 'NONE', #3819, .T. ) ;
#5644=DIRECTION ( 'NONE',  ( 0.000000000000000000, 0.000000000000000000, -1.000000000000000000 ) ) ;
#5645=LINE ( 'NONE', #20535, #22376 ) ;
#5665=CIRCLE ( 'NONE', #19306, 6.050000000006051870 ) ;
#5689=EDGE_LOOP ( 'NONE', ( #6694, #15031, #19094, #1460 ) ) ;
#5706=VERTEX_POINT ( 'NONE', #20056 ) ;
#5716=PRODUCT_DEFINITION_FORMATION_WITH_SPECIFIED_SOURCE ( 'ANY', '', #16053, .NOT_KNOWN. ) ;
#5740=DIRECTION ( 'NONE',  ( -1.000000000000000000, 0.000000000000000000, -0.000000000000000000 ) ) ;
#5788=CARTESIAN_POINT ( 'NONE',  ( 0.000000000000000000, 14.21257171757157955, -0.08908218613038007549 ) ) ;
#5794=VERTEX_POINT ( 'NONE', #18107 ) ;
#5860=EDGE_LOOP ( 'NONE', ( #11123, #6742, #23832, #2602 ) ) ;
#5875=CARTESIAN_POINT ( 'NONE',  ( 0.000000000000000000, 11.90821470209324140, 7.758837095328885880 ) ) ;
#5903=DIRECTION ( 'NONE',  ( -1.000000000000000000, 0.000000000000000000, 0.000000000000000000 ) ) ;
#5931=FACE_OUTER_BOUND ( 'NONE', #15192, .T. ) ;
#5942=VERTEX_POINT ( 'NONE', #9304 ) ;
#5951=CARTESIAN_POINT ( 'NONE',  ( 0.000000000000000000, -1.934484387512043435, 14.08058594723506474 ) ) ;
#5978=CARTESIAN_POINT ( 'NONE',  ( 0.000000000000000000, 0.000000000000000000, 0.000000000000000000 ) ) ;
#5995=DIRECTION ( 'NONE',  ( 0.000000000000000000, 0.000000000000000000, -1.000000000000000000 ) ) ;
#5997=CARTESIAN_POINT ( 'NONE',  ( 0.000000000000000000, 0.000000000000000000, 0.000000000000000000 ) ) ;
#6003=ORIENTED_EDGE ( 'NONE', *, *, #13421, .T. ) ;
#6008=VERTEX_POINT ( 'NONE', #7712 ) ;
#6023=DIRECTION ( 'NONE',  ( -1.000000000000000000, -0.000000000000000000, -0.000000000000000000 ) ) ;
#6025=DIRECTION ( 'NONE',  ( -1.000000000000000000, -0.000000000000000000, -0.000000000000000000 ) ) ;
#6041=EDGE_CURVE ( 'NONE', #21399, #20932, #13721, .T. ) ;
#6046=EDGE_CURVE ( 'NONE', #4844, #12989, #11242, .T. ) ;
#6059=CYLINDRICAL_SURFACE ( 'NONE', #7476, 11.68650000001168721 ) ;
#6076=EDGE_CURVE ( 'NONE', #6155, #3367, #9662, .T. ) ;
#6114=DIRECTION ( 'NONE',  ( 0.000000000000000000, 0.000000000000000000, 1.000000000000000000 ) ) ;
#6115=CIRCLE ( 'NONE', #16632, 6.050000000006051870 ) ;
#6119=FACE_OUTER_BOUND ( 'NONE', #23158, .T. ) ;
#6134=ORIENTED_EDGE ( 'NONE', *, *, #2573, .T. ) ;
#6145=CARTESIAN_POINT ( 'NONE',  ( 23.00000000000000000, -2.110835303355385051, 14.05523051341064722 ) ) ;
#6146=DIRECTION ( 'NONE',  ( -1.000000000000000000, 0.000000000000000000, -0.000000000000000000 ) ) ;
#6155=VERTEX_POINT ( 'NONE', #2728 ) ;
#6159=EDGE_LOOP ( 'NONE', ( #19727, #1611, #8882, #21467 ) ) ;
#6172=DIRECTION ( 'NONE',  ( 0.000000000000000000, 0.000000000000000000, -1.000000000000000000 ) ) ;
#6200=VERTEX_POINT ( 'NONE', #16013 ) ;
#6216=ORIENTED_EDGE ( 'NONE', *, *, #930, .F. ) ;
#6222=CARTESIAN_POINT ( 'NONE',  ( 23.00000000000000000, 0.000000000000000000, 0.000000000000000000 ) ) ;
#6236=EDGE_CURVE ( 'NONE', #18646, #7231, #3263, .T. ) ;
#6278=ORIENTED_EDGE ( 'NONE', *, *, #8969, .F. ) ;
#6287=DIRECTION ( 'NONE',  ( 0.000000000000000000, 0.000000000000000000, -1.000000000000000000 ) ) ;
#6304=ORIENTED_EDGE ( 'NONE', *, *, #18409, .F. ) ;
#6313=CARTESIAN_POINT ( 'NONE',  ( 23.00000000000000000, -10.66755332433025139, 4.772587172891002538 ) ) ;
#6324=AXIS2_PLACEMENT_3D ( 'NONE', #20054, #5052, #2849 ) ;
#6330=DIRECTION ( 'NONE',  ( -1.000000000000000000, 0.000000000000000000, 0.000000000000000000 ) ) ;
#6338=AXIS2_PLACEMENT_3D ( 'NONE', #21985, #5269, #18209 ) ;
#6341=AXIS2_PLACEMENT_3D ( 'NONE', #22238, #12714, #1618 ) ;
#6342=ADVANCED_FACE ( 'NONE', ( #12233, #10515 ), #2982, .F. ) ;
#6348=EDGE_CURVE ( 'NONE', #8876, #22006, #24060, .T. ) ;
#6350=ORIENTED_EDGE ( 'NONE', *, *, #12830, .F. ) ;
#6364=VECTOR ( 'NONE', #18976, 1000.000000000000000 ) ;
#6372=EDGE_CURVE ( 'NONE', #12689, #13734, #20640, .T. ) ;
#6377=ORIENTED_EDGE ( 'NONE', *, *, #11233, .F. ) ;
#6392=EDGE_LOOP ( 'NONE', ( #2954, #8371, #3616, #15892 ) ) ;
#6401=ORIENTED_EDGE ( 'NONE', *, *, #6372, .F. ) ;
#6413=DIRECTION ( 'NONE',  ( 0.000000000000000000, 0.000000000000000000, -1.000000000000000000 ) ) ;
#6423=ORIENTED_EDGE ( 'NONE', *, *, #23556, .T. ) ;
#6426=MECHANICAL_DESIGN_GEOMETRIC_PRESENTATION_REPRESENTATION('',(#12636),#15344);
#6429=CYLINDRICAL_SURFACE ( 'NONE', #21023, 6.050000000006051870 ) ;
#6449=AXIS2_PLACEMENT_3D ( 'NONE', #20722, #11791, #4143 ) ;
#6468=EDGE_CURVE ( 'NONE', #14984, #16640, #13743, .T. ) ;
#6471=AXIS2_PLACEMENT_3D ( 'NONE', #1177, #4968, #17887 ) ;
#6485=ORIENTED_EDGE ( 'NONE', *, *, #11233, .T. ) ;
#6487=CYLINDRICAL_SURFACE ( 'NONE', #16109, 17.87500000001787726 ) ;
#6491=EDGE_CURVE ( 'NONE', #18644, #13723, #20284, .T. ) ;
#6503=EDGE_CURVE ( 'NONE', #13734, #23514, #9063, .T. ) ;
#6533=EDGE_CURVE ( 'NONE', #10574, #5706, #11834, .T. ) ;
#6543=ORIENTED_EDGE ( 'NONE', *, *, #6041, .T. ) ;
#6546=LINE ( 'NONE', #8586, #17505 ) ;
#6561=ORIENTED_EDGE ( 'NONE', *, *, #9676, .F. ) ;
#6574=CARTESIAN_POINT ( 'NONE',  ( 23.00000000000000000, 12.00453763395396756, -7.608955687739546114 ) ) ;
#6600=EDGE_LOOP ( 'NONE', ( #4629, #12273, #21022, #14372 ) ) ;
#6604=ORIENTED_EDGE ( 'NONE', *, *, #930, .T. ) ;
#6610=ORIENTED_EDGE ( 'NONE', *, *, #18248, .F. ) ;
#6611=DIRECTION ( 'NONE',  ( 0.000000000000000000, 0.5406408174555987767, -0.8412535328311804284 ) ) ;
#6626=AXIS2_PLACEMENT_3D ( 'NONE', #1547, #3374, #1314 ) ;
#6631=EDGE_CURVE ( 'NONE', #14710, #9726, #5176, .T. ) ;
#6641=ORIENTED_EDGE ( 'NONE', *, *, #10765, .T. ) ;
#6642=DIRECTION ( 'NONE',  ( 1.000000000000000000, 0.000000000000000000, 0.000000000000000000 ) ) ;
#6650=ORIENTED_EDGE ( 'NONE', *, *, #2767, .F. ) ;
#6658=ADVANCED_FACE ( 'NONE', ( #17337 ), #641, .T. ) ;
#6684=UNCERTAINTY_MEASURE_WITH_UNIT (LENGTH_MEASURE( 1.000000000000000082E-05 ), #10220, 'distance_accuracy_value', 'NONE');
#6688=CYLINDRICAL_SURFACE ( 'NONE', #12384, 6.050000000006050982 ) ;
#6694=ORIENTED_EDGE ( 'NONE', *, *, #17819, .F. ) ;
#6699=ORIENTED_EDGE ( 'NONE', *, *, #19778, .F. ) ;
#6710=AXIS2_PLACEMENT_3D ( 'NONE', #15709, #970, #19507 ) ;
#6723=DIRECTION ( 'NONE',  ( 0.000000000000000000, 0.9898214418809322401, 0.1423148382732887240 ) ) ;
#6731=CIRCLE ( 'NONE', #22319, 17.87500000001787726 ) ;
#6734=DIRECTION ( 'NONE',  ( 0.000000000000000000, 0.5406408174555987767, -0.8412535328311804284 ) ) ;
#6742=ORIENTED_EDGE ( 'NONE', *, *, #894, .F. ) ;
#6751=ORIENTED_EDGE ( 'NONE', *, *, #5515, .F. ) ;
#6772=ORIENTED_EDGE ( 'NONE', *, *, #9208, .F. ) ;
#6773=VECTOR ( 'NONE', #309, 1000.000000000000000 ) ;
#6783=FACE_OUTER_BOUND ( 'NONE', #14250, .T. ) ;
#6823=VERTEX_POINT ( 'NONE', #21715 ) ;
#6857=DIRECTION ( 'NONE',  ( 0.000000000000000000, 0.000000000000000000, 1.000000000000000000 ) ) ;
#6858=EDGE_CURVE ( 'NONE', #20829, #18077, #11537, .T. ) ;
#6864=FACE_OUTER_BOUND ( 'NONE', #17311, .T. ) ;
#6866=AXIS2_PLACEMENT_3D ( 'NONE', #11414, #5594, #18889 ) ;
#6879=EDGE_CURVE ( 'NONE', #1756, #18646, #7138, .T. ) ;
#6897=CIRCLE ( 'NONE', #20533, 17.87500000001787726 ) ;
#6944=FACE_OUTER_BOUND ( 'NONE', #22022, .T. ) ;
#6961=EDGE_LOOP ( 'NONE', ( #10325, #1278, #15792, #19583, #13626, #2626, #611, #8373, #4980, #8069, #2137, #1972, #16383, #14943, #10292, #23116, #11544, #3087, #11073, #4585, #9358, #1100, #6604, #5226, #7334, #16981, #14809, #11077, #1466, #9183, #19231, #2737, #22581, #5130, #19920, #19222, #9723, #21714, #7125, #21223, #22819, #10507, #2288, #12932, #22809, #8936, #1191, #22734 ) ) ;
#6970=ORIENTED_EDGE ( 'NONE', *, *, #19932, .T. ) ;
#6972=ORIENTED_EDGE ( 'NONE', *, *, #12992, .F. ) ;
#6979=CARTESIAN_POINT ( 'NONE',  ( 0.000000000000000000, 0.000000000000000000, 0.000000000000000000 ) ) ;
#6985=ORIENTED_EDGE ( 'NONE', *, *, #18967, .T. ) ;
#6988=ORIENTED_EDGE ( 'NONE', *, *, #7892, .F. ) ;
#7000=DIRECTION ( 'NONE',  ( -1.000000000000000000, -0.000000000000000000, 0.000000000000000000 ) ) ;
#7001=DIRECTION ( 'NONE',  ( 0.000000000000000000, -0.9096319953545137782, -0.4154150130018967602 ) ) ;
#7010=FACE_OUTER_BOUND ( 'NONE', #18085, .T. ) ;
#7018=ORIENTED_EDGE ( 'NONE', *, *, #3056, .T. ) ;
#7020=VERTEX_POINT ( 'NONE', #9308 ) ;
#7031=DIRECTION ( 'NONE',  ( -1.000000000000000000, -0.000000000000000000, -0.000000000000000000 ) ) ;
#7038=DIRECTION ( 'NONE',  ( 0.000000000000000000, 0.000000000000000000, 1.000000000000000000 ) ) ;
#7039=( NAMED_UNIT ( * ) PLANE_ANGLE_UNIT ( ) SI_UNIT ( $, .RADIAN. ) );
#7071=EDGE_CURVE ( 'NONE', #11063, #12041, #9416, .T. ) ;
#7099=CARTESIAN_POINT ( 'NONE',  ( 11.50000000000000000, 2.119223430970168298, 17.74893002550480858 ) ) ;
#7117=VECTOR ( 'NONE', #21111, 1000.000000000000000 ) ;
#7125=ORIENTED_EDGE ( 'NONE', *, *, #3973, .T. ) ;
#7138=CIRCLE ( 'NONE', #9835, 6.050000000006051870 ) ;
#7164=CARTESIAN_POINT ( 'NONE',  ( 0.000000000000000000, 0.000000000000000000, 0.000000000000000000 ) ) ;
#7178=( NAMED_UNIT ( * ) SI_UNIT ( $, .STERADIAN. ) SOLID_ANGLE_UNIT ( ) );
#7198=CIRCLE ( 'NONE', #14214, 6.050000000006050094 ) ;
#7204=EDGE_LOOP ( 'NONE', ( #8521, #5588, #18365, #9618 ) ) ;
#7207=CARTESIAN_POINT ( 'NONE',  ( 23.00000000000000000, 0.000000000000000000, 0.000000000000000000 ) ) ;
#7217=ORIENTED_EDGE ( 'NONE', *, *, #12294, .F. ) ;
#7225=AXIS2_PLACEMENT_3D ( 'NONE', #17421, #10079, #719 ) ;
#7231=VERTEX_POINT ( 'NONE', #21410 ) ;
#7240=CIRCLE ( 'NONE', #13475, 6.050000000006050094 ) ;
#7252=AXIS2_PLACEMENT_3D ( 'NONE', #714, #19384, #2657 ) ;
#7260=DIRECTION ( 'NONE',  ( 0.000000000000000000, -0.2817325568414367765, 0.9594929736144953702 ) ) ;
#7280=ORIENTED_EDGE ( 'NONE', *, *, #20717, .F. ) ;
#7291=EDGE_LOOP ( 'NONE', ( #1420, #17515, #18907, #180 ) ) ;
#7297=CYLINDRICAL_SURFACE ( 'NONE', #12669, 11.68650000001168721 ) ;
#7313=DIRECTION ( 'NONE',  ( -1.000000000000000000, 0.000000000000000000, -0.000000000000000000 ) ) ;
#7334=ORIENTED_EDGE ( 'NONE', *, *, #20014, .F. ) ;
#7336=ORIENTED_EDGE ( 'NONE', *, *, #7892, .T. ) ;
#7338=CARTESIAN_POINT ( 'NONE',  ( 11.49999999999999822, 12.02595010061972403, -13.22467954916274913 ) ) ;
#7357=EDGE_LOOP ( 'NONE', ( #8810, #10659, #6641, #19790 ) ) ;
#7382=CARTESIAN_POINT ( 'NONE',  ( 23.00000000000000000, -13.61176534793449200, 4.089617900950054619 ) ) ;
#7387=ORIENTED_EDGE ( 'NONE', *, *, #9149, .F. ) ;
#7400=ORIENTED_EDGE ( 'NONE', *, *, #8322, .F. ) ;
#7422=EDGE_LOOP ( 'NONE', ( #15684, #229, #6772, #7336 ) ) ;
#7466=CARTESIAN_POINT ( 'NONE',  ( 23.00000000000000000, -1.934484387512043435, 14.08058594723506474 ) ) ;
#7476=AXIS2_PLACEMENT_3D ( 'NONE', #8104, #2385, #11264 ) ;
#7478=AXIS2_PLACEMENT_3D ( 'NONE', #8160, #13797, #2812 ) ;
#7505=DIRECTION ( 'NONE',  ( -1.000000000000000000, 0.000000000000000000, 0.000000000000000000 ) ) ;
#7525=AXIS2_PLACEMENT_3D ( 'NONE', #13724, #22638, #21173 ) ;
#7530=CARTESIAN_POINT ( 'NONE',  ( -10.00000000000000000, 0.000000000000000000, 0.000000000000000000 ) ) ;
#7533=EDGE_CURVE ( 'NONE', #22050, #20652, #3925, .T. ) ;
#7545=ORIENTED_EDGE ( 'NONE', *, *, #18701, .T. ) ;
#7562=DIRECTION ( 'NONE',  ( 0.000000000000000000, 0.000000000000000000, 1.000000000000000000 ) ) ;
#7569=DIRECTION ( 'NONE',  ( 0.000000000000000000, 0.000000000000000000, 1.000000000000000000 ) ) ;
#7589=ORIENTED_EDGE ( 'NONE', *, *, #6858, .T. ) ;
#7590=EDGE_CURVE ( 'NONE', #23563, #16008, #4405, .T. ) ;
#7591=ADVANCED_FACE ( 'NONE', ( #20404 ), #289, .T. ) ;
#7612=VECTOR ( 'NONE', #15062, 1000.000000000000000 ) ;
#7629=CARTESIAN_POINT ( 'NONE',  ( 23.00000000000000000, 14.21257171757157245, 0.08908218613057176938 ) ) ;
#7640=VERTEX_POINT ( 'NONE', #22494 ) ;
#7650=ADVANCED_FACE ( 'NONE', ( #18082 ), #3075, .T. ) ;
#7652=ORIENTED_EDGE ( 'NONE', *, *, #18189, .T. ) ;
#7664=ORIENTED_EDGE ( 'NONE', *, *, #14769, .T. ) ;
#7676=ORIENTED_EDGE ( 'NONE', *, *, #9515, .F. ) ;
#7698=ORIENTED_EDGE ( 'NONE', *, *, #7533, .F. ) ;
#7712=CARTESIAN_POINT ( 'NONE',  ( 0.000000000000000000, -7.033831428820064069, -16.43291941292179104 ) ) ;
#7713=CARTESIAN_POINT ( 'NONE',  ( 23.00000000000000000, 12.02595010061954284, 13.22467954916291433 ) ) ;
#7714=AXIS2_PLACEMENT_3D ( 'NONE', #11696, #22844, #15119 ) ;
#7720=DIRECTION ( 'NONE',  ( -1.000000000000000000, -0.000000000000000000, 0.000000000000000000 ) ) ;
#7721=ORIENTED_EDGE ( 'NONE', *, *, #993, .F. ) ;
#7737=DIRECTION ( 'NONE',  ( -1.000000000000000000, 0.000000000000000000, 0.000000000000000000 ) ) ;
#7743=CARTESIAN_POINT ( 'NONE',  ( 0.000000000000000000, 0.000000000000000000, 0.000000000000000000 ) ) ;
#7764=FACE_OUTER_BOUND ( 'NONE', #9396, .T. ) ;
#7800=ORIENTED_EDGE ( 'NONE', *, *, #14252, .T. ) ;
#7824=DIRECTION ( 'NONE',  ( 1.000000000000000000, 0.000000000000000000, 0.000000000000000000 ) ) ;
#7835=ORIENTED_EDGE ( 'NONE', *, *, #10039, .T. ) ;
#7849=DIRECTION ( 'NONE',  ( -1.000000000000000000, -0.000000000000000000, -0.000000000000000000 ) ) ;
#7850=ORIENTED_EDGE ( 'NONE', *, *, #16126, .T. ) ;
#7859=CIRCLE ( 'NONE', #6338, 17.87500000001787726 ) ;
#7872=UNCERTAINTY_MEASURE_WITH_UNIT (LENGTH_MEASURE( 1.000000000000000082E-05 ), #3623, 'distance_accuracy_value', 'NONE');
#7892=EDGE_CURVE ( 'NONE', #9833, #8545, #12565, .T. ) ;
#7904=CARTESIAN_POINT ( 'NONE',  ( 23.00000000000000000, 5.823083658124710738, 12.96521604808350503 ) ) ;
#7924=DIRECTION ( 'NONE',  ( 1.000000000000000000, -0.000000000000000000, 0.000000000000000000 ) ) ;
#7925=DIRECTION ( 'NONE',  ( 0.000000000000000000, 0.000000000000000000, -1.000000000000000000 ) ) ;
#7944=ORIENTED_EDGE ( 'NONE', *, *, #14252, .F. ) ;
#7945=AXIS2_PLACEMENT_3D ( 'NONE', #17918, #4633, #12034 ) ;
#7948=ADVANCED_FACE ( 'NONE', ( #7010 ), #19951, .T. ) ;
#7969=ORIENTED_EDGE ( 'NONE', *, *, #17360, .F. ) ;
#7987=AXIS2_PLACEMENT_3D ( 'NONE', #15028, #5525, #23967 ) ;
#7993=DIRECTION ( 'NONE',  ( -1.000000000000000000, 0.000000000000000000, 0.000000000000000000 ) ) ;
#7995=CARTESIAN_POINT ( 'NONE',  ( -10.00000000000000000, 0.000000000000000000, 0.000000000000000000 ) ) ;
#8005=AXIS2_PLACEMENT_3D ( 'NONE', #5978, #22344, #13412 ) ;
#8006=CARTESIAN_POINT ( 'NONE',  ( 11.50000000000000000, -14.80154252341802490, 10.02147513732818851 ) ) ;
#8015=CARTESIAN_POINT ( 'NONE',  ( 23.00000000000000000, -13.66196005206961850, -3.918670437617226110 ) ) ;
#8029=DIRECTION ( 'NONE',  ( 0.000000000000000000, 0.2817325568414237313, 0.9594929736144991450 ) ) ;
#8050=CARTESIAN_POINT ( 'NONE',  ( 23.00000000000000000, 0.000000000000000000, 0.000000000000000000 ) ) ;
#8066=DIRECTION ( 'NONE',  ( 0.000000000000000000, 0.9898214418809322401, 0.1423148382732887240 ) ) ;
#8069=ORIENTED_EDGE ( 'NONE', *, *, #1473, .T. ) ;
#8081=DIRECTION ( 'NONE',  ( -1.000000000000000000, -0.000000000000000000, 0.000000000000000000 ) ) ;
#8082=ORIENTED_EDGE ( 'NONE', *, *, #5021, .F. ) ;
#8090=EDGE_CURVE ( 'NONE', #21740, #5942, #4419, .T. ) ;
#8104=CARTESIAN_POINT ( 'NONE',  ( 23.00000000000000000, 0.000000000000000000, 0.000000000000000000 ) ) ;
#8114=DIRECTION ( 'NONE',  ( -1.000000000000000000, -0.000000000000000000, -0.000000000000000000 ) ) ;
#8124=VERTEX_POINT ( 'NONE', #12325 ) ;
#8127=CARTESIAN_POINT ( 'NONE',  ( -10.00000000000000000, 0.000000000000000000, 0.000000000000000000 ) ) ;
#8160=CARTESIAN_POINT ( 'NONE',  ( 0.000000000000000000, -13.66196005206961850, -3.918670437617226110 ) ) ;
#8172=EDGE_CURVE ( 'NONE', #15320, #6823, #22958, .T. ) ;
#8248=DIRECTION ( 'NONE',  ( -1.000000000000000000, -0.000000000000000000, -0.000000000000000000 ) ) ;
#8257=LINE ( 'NONE', #2304, #9404 ) ;
#8258=AXIS2_PLACEMENT_3D ( 'NONE', #15779, #2847, #10022 ) ;
#8260=AXIS2_PLACEMENT_3D ( 'NONE', #10411, #3920, #10974 ) ;
#8280=CARTESIAN_POINT ( 'NONE',  ( 50.00005079999999680, 0.000000000000000000, 0.000000000000000000 ) ) ;
#8318=CIRCLE ( 'NONE', #16116, 6.050000000006052758 ) ;
#8321=AXIS2_PLACEMENT_3D ( 'NONE', #2247, #5903, #18975 ) ;
#8322=EDGE_CURVE ( 'NONE', #19925, #2741, #19213, .T. ) ;
#8326=LINE ( 'NONE', #16257, #12765 ) ;
#8371=ORIENTED_EDGE ( 'NONE', *, *, #20335, .F. ) ;
#8373=ORIENTED_EDGE ( 'NONE', *, *, #22832, .T. ) ;
#8391=FACE_OUTER_BOUND ( 'NONE', #7291, .T. ) ;
#8399=CIRCLE ( 'NONE', #13074, 11.68650000001168898 ) ;
#8412=DIRECTION ( 'NONE',  ( 1.000000000000000000, 0.000000000000000000, 0.000000000000000000 ) ) ;
#8414=ORIENTED_EDGE ( 'NONE', *, *, #11688, .F. ) ;
#8440=CIRCLE ( 'NONE', #22101, 11.68650000001168721 ) ;
#8446=VERTEX_POINT ( 'NONE', #4637 ) ;
#8463=EDGE_CURVE ( 'NONE', #2741, #18301, #20779, .T. ) ;
#8482=DIRECTION ( 'NONE',  ( 1.000000000000000000, -0.000000000000000000, -0.000000000000000000 ) ) ;
#8492=EDGE_CURVE ( 'NONE', #23530, #21399, #9844, .T. ) ;
#8518=CARTESIAN_POINT ( 'NONE',  ( 11.50000000000000000, 2.967071445749915437, 17.62702788437274393 ) ) ;
#8521=ORIENTED_EDGE ( 'NONE', *, *, #8641, .F. ) ;
#8527=ORIENTED_EDGE ( 'NONE', *, *, #3191, .F. ) ;
#8528=CARTESIAN_POINT ( 'NONE',  ( 11.50000000000000000, 2.967071445750145919, -17.62702788437270840 ) ) ;
#8534=PRODUCT_DEFINITION ( 'UNKNOWN', '', #5716, #11865 ) ;
#8541=ADVANCED_FACE ( 'NONE', ( #2670 ), #21082, .T. ) ;
#8545=VERTEX_POINT ( 'NONE', #20229 ) ;
#8568=DIRECTION ( 'NONE',  ( 0.000000000000000000, 0.2817325568414237313, 0.9594929736144991450 ) ) ;
#8578=CIRCLE ( 'NONE', #12867, 9.000000000000000000 ) ;
#8581=EDGE_CURVE ( 'NONE', #6008, #22050, #10627, .T. ) ;
#8586=CARTESIAN_POINT ( 'NONE',  ( 23.00000000000000000, 11.58003564732003277, -1.573866785045813010 ) ) ;
#8613=DIRECTION ( 'NONE',  ( 0.000000000000000000, 0.000000000000000000, 1.000000000000000000 ) ) ;
#8629=VERTEX_POINT ( 'NONE', #16074 ) ;
#8641=EDGE_CURVE ( 'NONE', #18942, #1347, #21818, .T. ) ;
#8645=VECTOR ( 'NONE', #9410, 1000.000000000000000 ) ;
#8658=ORIENTED_EDGE ( 'NONE', *, *, #23643, .T. ) ;
#8672=ADVANCED_FACE ( 'NONE', ( #20117 ), #3393, .T. ) ;
#8680=AXIS2_PLACEMENT_3D ( 'NONE', #15203, #3654, #2305 ) ;
#8682=VECTOR ( 'NONE', #22253, 1000.000000000000000 ) ;
#8700=VERTEX_POINT ( 'NONE', #2023 ) ;
#8726=CIRCLE ( 'NONE', #10669, 6.050000000006050982 ) ;
#8744=AXIS2_PLACEMENT_3D ( 'NONE', #7995, #2276, #20952 ) ;
#8763=DIRECTION ( 'NONE',  ( 0.000000000000000000, 0.000000000000000000, 1.000000000000000000 ) ) ;
#8764=CIRCLE ( 'NONE', #19687, 6.050000000006050982 ) ;
#8776=ADVANCED_FACE ( 'NONE', ( #5931 ), #22427, .T. ) ;
#8777=CIRCLE ( 'NONE', #18540, 6.050000000006052758 ) ;
#8783=EDGE_LOOP ( 'NONE', ( #9081, #8957, #6278, #6610 ) ) ;
#8810=ORIENTED_EDGE ( 'NONE', *, *, #7533, .T. ) ;
#8837=VERTEX_POINT ( 'NONE', #11762 ) ;
#8865=CARTESIAN_POINT ( 'NONE',  ( 0.000000000000000000, 0.000000000000000000, 9.000000000000000000 ) ) ;
#8876=VERTEX_POINT ( 'NONE', #19441 ) ;
#8882=ORIENTED_EDGE ( 'NONE', *, *, #19095, .T. ) ;
#8891=FACE_OUTER_BOUND ( 'NONE', #19921, .T. ) ;
#8900=CARTESIAN_POINT ( 'NONE',  ( 0.000000000000000000, 3.378881074890309311, 11.18737882312122878 ) ) ;
#8906=DIRECTION ( 'NONE',  ( -1.000000000000000000, 0.000000000000000000, 0.000000000000000000 ) ) ;
#8909=ORIENTED_EDGE ( 'NONE', *, *, #17360, .T. ) ;
#8935=ORIENTED_EDGE ( 'NONE', *, *, #4431, .F. ) ;
#8936=ORIENTED_EDGE ( 'NONE', *, *, #17660, .F. ) ;
#8949=DIRECTION ( 'NONE',  ( 0.000000000000000000, 0.000000000000000000, 1.000000000000000000 ) ) ;
#8955=DIRECTION ( 'NONE',  ( -1.000000000000000000, -0.000000000000000000, 0.000000000000000000 ) ) ;
#8957=ORIENTED_EDGE ( 'NONE', *, *, #8322, .T. ) ;
#8969=EDGE_CURVE ( 'NONE', #9146, #2741, #4037, .T. ) ;
#9007=ORIENTED_EDGE ( 'NONE', *, *, #21131, .F. ) ;
#9012=CARTESIAN_POINT ( 'NONE',  ( 23.00000000000000000, -13.66196005206961850, -3.918670437617226110 ) ) ;
#9019=DIRECTION ( 'NONE',  ( -1.000000000000000000, 0.000000000000000000, 0.000000000000000000 ) ) ;
#9063=CIRCLE ( 'NONE', #6341, 6.050000000006050094 ) ;
#9081=ORIENTED_EDGE ( 'NONE', *, *, #14208, .F. ) ;
#9146=VERTEX_POINT ( 'NONE', #21212 ) ;
#9149=EDGE_CURVE ( 'NONE', #15083, #22027, #468, .T. ) ;
#9153=AXIS2_PLACEMENT_3D ( 'NONE', #5951, #17292, #19502 ) ;
#9162=DIRECTION ( 'NONE',  ( -1.000000000000000000, 0.000000000000000000, 0.000000000000000000 ) ) ;
#9171=ORIENTED_EDGE ( 'NONE', *, *, #12174, .F. ) ;
#9183=ORIENTED_EDGE ( 'NONE', *, *, #6631, .T. ) ;
#9186=CARTESIAN_POINT ( 'NONE',  ( 0.000000000000000000, 11.37860023611358962, -13.78561139983841599 ) ) ;
#9201=CARTESIAN_POINT ( 'NONE',  ( 23.00000000000000000, -2.110835303355205639, -14.05523051341068097 ) ) ;
#9208=EDGE_CURVE ( 'NONE', #9833, #1756, #19391, .T. ) ;
#9220=CARTESIAN_POINT ( 'NONE',  ( 23.00000000000000000, -13.66196005206961850, 2.131329562388824428 ) ) ;
#9222=DIRECTION ( 'NONE',  ( 0.000000000000000000, 0.000000000000000000, -1.000000000000000000 ) ) ;
#9229=DIRECTION ( 'NONE',  ( 0.000000000000000000, 0.000000000000000000, 1.000000000000000000 ) ) ;
#9237=ORIENTED_EDGE ( 'NONE', *, *, #6046, .F. ) ;
#9238=ORIENTED_EDGE ( 'NONE', *, *, #8463, .T. ) ;
#9259=ORIENTED_EDGE ( 'NONE', *, *, #8581, .F. ) ;
#9276=VERTEX_POINT ( 'NONE', #5093 ) ;
#9284=DIRECTION ( 'NONE',  ( 0.000000000000000000, 0.000000000000000000, 1.000000000000000000 ) ) ;
#9285=CARTESIAN_POINT ( 'NONE',  ( -10.00000000000000000, 0.000000000000000000, 0.000000000000000000 ) ) ;
#9304=CARTESIAN_POINT ( 'NONE',  ( 0.000000000000000000, -13.66196005206961850, 2.131329562388824428 ) ) ;
#9308=CARTESIAN_POINT ( 'NONE',  ( 23.00000000000000000, -14.80154252341789700, -10.02147513732837680 ) ) ;
#9358=ORIENTED_EDGE ( 'NONE', *, *, #12454, .F. ) ;
#9365=DIRECTION ( 'NONE',  ( 0.000000000000000000, 0.000000000000000000, 1.000000000000000000 ) ) ;
#9368=EDGE_CURVE ( 'NONE', #18644, #21399, #10987, .T. ) ;
#9396=EDGE_LOOP ( 'NONE', ( #22733, #6543, #24059, #7018 ) ) ;
#9404=VECTOR ( 'NONE', #4380, 1000.000000000000000 ) ;
#9410=DIRECTION ( 'NONE',  ( -1.000000000000000000, 0.000000000000000000, 0.000000000000000000 ) ) ;
#9416=LINE ( 'NONE', #2248, #6364 ) ;
#9439=APPLICATION_CONTEXT ( 'automotive_design' ) ;
#9461=VERTEX_POINT ( 'NONE', #8865 ) ;
#9465=DIRECTION ( 'NONE',  ( -1.000000000000000000, 0.000000000000000000, -0.000000000000000000 ) ) ;
#9477=DIRECTION ( 'NONE',  ( -1.000000000000000000, -0.000000000000000000, 0.000000000000000000 ) ) ;
#9479=FACE_OUTER_BOUND ( 'NONE', #921, .T. ) ;
#9481=CARTESIAN_POINT ( 'NONE',  ( 23.00000000000000000, -11.55437235128772500, -1.752358929577761515 ) ) ;
#9515=EDGE_CURVE ( 'NONE', #20283, #8446, #16774, .T. ) ;
#9529=EDGE_LOOP ( 'NONE', ( #9940, #7652, #21287, #12968 ) ) ;
#9542=ADVANCED_FACE ( 'NONE', ( #3976 ), #6059, .T. ) ;
#9568=AXIS2_PLACEMENT_3D ( 'NONE', #987, #8412, #15863 ) ;
#9571=CARTESIAN_POINT ( 'NONE',  ( 0.000000000000000000, 2.967071445749915881, 17.62702788437274393 ) ) ;
#9608=EDGE_CURVE ( 'NONE', #23202, #3712, #21953, .T. ) ;
#9617=DIRECTION ( 'NONE',  ( -1.000000000000000000, 0.000000000000000000, 0.000000000000000000 ) ) ;
#9618=ORIENTED_EDGE ( 'NONE', *, *, #20780, .T. ) ;
#9658=DIRECTION ( 'NONE',  ( -1.000000000000000000, 0.000000000000000000, -0.000000000000000000 ) ) ;
#9662=LINE ( 'NONE', #2615, #13328 ) ;
#9663=FACE_OUTER_BOUND ( 'NONE', #4079, .T. ) ;
#9676=EDGE_CURVE ( 'NONE', #6823, #12689, #14532, .T. ) ;
#9679=ORIENTED_EDGE ( 'NONE', *, *, #5311, .T. ) ;
#9706=CARTESIAN_POINT ( 'NONE',  ( 0.000000000000000000, 14.21257171757157245, 0.08908218613057176938 ) ) ;
#9723=ORIENTED_EDGE ( 'NONE', *, *, #22586, .F. ) ;
#9726=VERTEX_POINT ( 'NONE', #17508 ) ;
#9730=EDGE_CURVE ( 'NONE', #18077, #15534, #10245, .T. ) ;
#9744=CARTESIAN_POINT ( 'NONE',  ( 0.000000000000000000, 12.00453763395397466, 7.608955687739546114 ) ) ;
#9745=CARTESIAN_POINT ( 'NONE',  ( 11.50000000000000000, 17.02535186363803632, 5.445458559199172655 ) ) ;
#9750=LINE ( 'NONE', #4558, #3911 ) ;
#9755=AXIS2_PLACEMENT_3D ( 'NONE', #1688, #1468, #5583 ) ;
#9833=VERTEX_POINT ( 'NONE', #18798 ) ;
#9835=AXIS2_PLACEMENT_3D ( 'NONE', #22784, #18878, #1809 ) ;
#9844=LINE ( 'NONE', #8518, #20391 ) ;
#9850=AXIS2_PLACEMENT_3D ( 'NONE', #14387, #14042, #23567 ) ;
#9866=DIRECTION ( 'NONE',  ( -1.000000000000000000, 0.000000000000000000, 0.000000000000000000 ) ) ;
#9887=CARTESIAN_POINT ( 'NONE',  ( 0.000000000000000000, 8.890849273385601492, 7.584660931657517757 ) ) ;
#9940=ORIENTED_EDGE ( 'NONE', *, *, #3191, .T. ) ;
#9943=CARTESIAN_POINT ( 'NONE',  ( 0.000000000000000000, -3.205857990849823480, 11.23818298448541420 ) ) ;
#9970=CARTESIAN_POINT ( 'NONE',  ( 23.00000000000000000, 5.823083658124882156, -12.96521604808343398 ) ) ;
#9990=ORIENTED_EDGE ( 'NONE', *, *, #20851, .T. ) ;
#10012=ADVANCED_FACE ( 'NONE', ( #13670 ), #6487, .T. ) ;
#10020=ORIENTED_EDGE ( 'NONE', *, *, #12294, .T. ) ;
#10022=DIRECTION ( 'NONE',  ( 0.000000000000000000, -0.5406408174555868973, -0.8412535328311879779 ) ) ;
#10039=EDGE_CURVE ( 'NONE', #8700, #20652, #18072, .T. ) ;
#10042=CARTESIAN_POINT ( 'NONE',  ( 0.000000000000000000, 10.59264252385236915, 4.936618945406632264 ) ) ;
#10061=CIRCLE ( 'NONE', #15936, 6.050000000006050982 ) ;
#10079=DIRECTION ( 'NONE',  ( -1.000000000000000000, -0.000000000000000000, 0.000000000000000000 ) ) ;
#10080=VECTOR ( 'NONE', #17526, 1000.000000000000000 ) ;
#10103=CYLINDRICAL_SURFACE ( 'NONE', #2192, 9.000000000000000000 ) ;
#10107=ORIENTED_EDGE ( 'NONE', *, *, #18189, .F. ) ;
#10115=ADVANCED_FACE ( 'NONE', ( #16232, #3169 ), #15874, .F. ) ;
#10160=DIRECTION ( 'NONE',  ( -1.000000000000000000, 0.000000000000000000, 0.000000000000000000 ) ) ;
#10183=AXIS2_PLACEMENT_3D ( 'NONE', #4010, #471, #11427 ) ;
#10191=ORIENTED_EDGE ( 'NONE', *, *, #22860, .T. ) ;
#10202=AXIS2_PLACEMENT_3D ( 'NONE', #19914, #12564, #23704 ) ;
#10215=EDGE_LOOP ( 'NONE', ( #3347, #6216, #11048, #3276 ) ) ;
#10220=( LENGTH_UNIT ( ) NAMED_UNIT ( * ) SI_UNIT ( .MILLI., .METRE. ) );
#10240=DIRECTION ( 'NONE',  ( -1.000000000000000000, 0.000000000000000000, 0.000000000000000000 ) ) ;
#10245=CIRCLE ( 'NONE', #14155, 11.68650000001168721 ) ;
#10253=ADVANCED_FACE ( 'NONE', ( #9479 ), #16937, .T. ) ;
#10261=LINE ( 'NONE', #428, #14988 ) ;
#10292=ORIENTED_EDGE ( 'NONE', *, *, #391, .T. ) ;
#10296=ORIENTED_EDGE ( 'NONE', *, *, #12992, .T. ) ;
#10321=ORIENTED_EDGE ( 'NONE', *, *, #10039, .F. ) ;
#10325=ORIENTED_EDGE ( 'NONE', *, *, #17, .T. ) ;
#10348=AXIS2_PLACEMENT_3D ( 'NONE', #14174, #1252, #1023 ) ;
#10350=AXIS2_PLACEMENT_3D ( 'NONE', #3524, #12312, #18053 ) ;
#10367=AXIS2_PLACEMENT_3D ( 'NONE', #13607, #17503, #804 ) ;
#10372=AXIS2_PLACEMENT_3D ( 'NONE', #432, #18988, #22895 ) ;
#10386=CIRCLE ( 'NONE', #19763, 6.050000000006052758 ) ;
#10411=CARTESIAN_POINT ( 'NONE',  ( 23.00000000000000000, 0.000000000000000000, 0.000000000000000000 ) ) ;
#10422=EDGE_CURVE ( 'NONE', #12203, #16008, #8257, .T. ) ;
#10440=LINE ( 'NONE', #17901, #15999 ) ;
#10448=ORIENTED_EDGE ( 'NONE', *, *, #8969, .T. ) ;
#10452=AXIS2_PLACEMENT_3D ( 'NONE', #17026, #7849, #6172 ) ;
#10463=DIRECTION ( 'NONE',  ( -1.000000000000000000, -0.000000000000000000, -0.000000000000000000 ) ) ;
#10495=ORIENTED_EDGE ( 'NONE', *, *, #391, .F. ) ;
#10507=ORIENTED_EDGE ( 'NONE', *, *, #8090, .F. ) ;
#10515=FACE_OUTER_BOUND ( 'NONE', #23293, .T. ) ;
#10527=ORIENTED_EDGE ( 'NONE', *, *, #6503, .T. ) ;
#10534=CARTESIAN_POINT ( 'NONE',  ( 0.000000000000000000, -13.66196005206966468, 3.918670437617043145 ) ) ;
#10574=VERTEX_POINT ( 'NONE', #18164 ) ;
#10586=AXIS2_PLACEMENT_3D ( 'NONE', #13528, #22928, #17425 ) ;
#10601=LINE ( 'NONE', #19423, #4294 ) ;
#10605=ORIENTED_EDGE ( 'NONE', *, *, #12454, .T. ) ;
#10611=ORIENTED_EDGE ( 'NONE', *, *, #13314, .F. ) ;
#10613=VECTOR ( 'NONE', #159, 1000.000000000000000 ) ;
#10627=CIRCLE ( 'NONE', #134, 17.87500000001787726 ) ;
#10638=CARTESIAN_POINT ( 'NONE',  ( 23.00000000000000000, 14.21257171757157955, -0.08908218613038007549 ) ) ;
#10642=ORIENTED_EDGE ( 'NONE', *, *, #20717, .T. ) ;
#10644=ADVANCED_FACE ( 'NONE', ( #14600 ), #11270, .T. ) ;
#10651=EDGE_CURVE ( 'NONE', #15821, #6200, #23050, .T. ) ;
#10659=ORIENTED_EDGE ( 'NONE', *, *, #24077, .T. ) ;
#10660=FACE_OUTER_BOUND ( 'NONE', #10902, .T. ) ;
#10669=AXIS2_PLACEMENT_3D ( 'NONE', #17486, #6642, #22992 ) ;
#10693=DIRECTION ( 'NONE',  ( -1.000000000000000000, 0.000000000000000000, 0.000000000000000000 ) ) ;
#10702=EDGE_LOOP ( 'NONE', ( #17519, #7387, #16531, #13271 ) ) ;
#10716=CARTESIAN_POINT ( 'NONE',  ( 11.50000000000000000, -7.033831428820292331, 16.43291941292170577 ) ) ;
#10736=ORIENTED_EDGE ( 'NONE', *, *, #6468, .T. ) ;
#10765=EDGE_CURVE ( 'NONE', #8837, #1531, #20339, .T. ) ;
#10776=VERTEX_POINT ( 'NONE', #9943 ) ;
#10828=LINE ( 'NONE', #10716, #1040 ) ;
#10859=LINE ( 'NONE', #12575, #20052 ) ;
#10896=CARTESIAN_POINT ( 'NONE',  ( 0.000000000000000000, 12.00453763395396756, -7.608955687739546114 ) ) ;
#10902=EDGE_LOOP ( 'NONE', ( #12088, #4615, #7800, #14162 ) ) ;
#10907=FACE_OUTER_BOUND ( 'NONE', #22700, .T. ) ;
#10926=DIRECTION ( 'NONE',  ( 0.000000000000000000, 0.000000000000000000, 1.000000000000000000 ) ) ;
#10931=DIRECTION ( 'NONE',  ( 0.000000000000000000, 0.000000000000000000, 1.000000000000000000 ) ) ;
#10932=CARTESIAN_POINT ( 'NONE',  ( 23.00000000000000000, 0.000000000000000000, 0.000000000000000000 ) ) ;
#10935=DIRECTION ( 'NONE',  ( 0.000000000000000000, 0.000000000000000000, 1.000000000000000000 ) ) ;
#10944=DIRECTION ( 'NONE',  ( -1.000000000000000000, -0.000000000000000000, -0.000000000000000000 ) ) ;
#10956=CARTESIAN_POINT ( 'NONE',  ( 23.00000000000000000, 14.21257171757157245, 6.139082186136624486 ) ) ;
#10962=EDGE_CURVE ( 'NONE', #20443, #18942, #21105, .T. ) ;
#10974=DIRECTION ( 'NONE',  ( -0.000000000000000000, 0.000000000000000000, 1.000000000000000000 ) ) ;
#10987=CIRCLE ( 'NONE', #12178, 17.87500000001787726 ) ;
#11005=CARTESIAN_POINT ( 'NONE',  ( 23.00000000000000000, 6.242160243097294448, -9.879763041175060323 ) ) ;
#11010=DIRECTION ( 'NONE',  ( -1.000000000000000000, 0.000000000000000000, 0.000000000000000000 ) ) ;
#11047=DIRECTION ( 'NONE',  ( -1.000000000000000000, -0.000000000000000000, -0.000000000000000000 ) ) ;
#11048=ORIENTED_EDGE ( 'NONE', *, *, #6076, .F. ) ;
#11063=VERTEX_POINT ( 'NONE', #11005 ) ;
#11071=AXIS2_PLACEMENT_3D ( 'NONE', #13896, #21077, #1953 ) ;
#11073=ORIENTED_EDGE ( 'NONE', *, *, #13289, .T. ) ;
#11077=ORIENTED_EDGE ( 'NONE', *, *, #18248, .T. ) ;
#11107=CYLINDRICAL_SURFACE ( 'NONE', #22234, 6.050000000006051870 ) ;
#11108=CARTESIAN_POINT ( 'NONE',  ( 11.50000000000000000, -7.812991839788663739, -16.07708877602020436 ) ) ;
#11112=CIRCLE ( 'NONE', #19731, 9.000000000000000000 ) ;
#11114=ORIENTED_EDGE ( 'NONE', *, *, #19778, .T. ) ;
#11116=VECTOR ( 'NONE', #21605, 1000.000000000000000 ) ;
#11123=ORIENTED_EDGE ( 'NONE', *, *, #19759, .F. ) ;
#11132=FACE_OUTER_BOUND ( 'NONE', #7357, .T. ) ;
#11152=CYLINDRICAL_SURFACE ( 'NONE', #14967, 6.050000000006050982 ) ;
#11156=VERTEX_POINT ( 'NONE', #19199 ) ;
#11168=EDGE_CURVE ( 'NONE', #7020, #20664, #3966, .T. ) ;
#11179=CARTESIAN_POINT ( 'NONE',  ( 23.00000000000000000, -0.09016380984471503157, 11.68615217844040544 ) ) ;
#11224=DIRECTION ( 'NONE',  ( -1.000000000000000000, 0.000000000000000000, 0.000000000000000000 ) ) ;
#11233=EDGE_CURVE ( 'NONE', #3225, #7640, #4759, .T. ) ;
#11236=CYLINDRICAL_SURFACE ( 'NONE', #15080, 6.050000000006050982 ) ;
#11242=LINE ( 'NONE', #12849, #8645 ) ;
#11246=ORIENTED_EDGE ( 'NONE', *, *, #8090, .T. ) ;
#11264=DIRECTION ( 'NONE',  ( 0.000000000000000000, 0.000000000000000000, 1.000000000000000000 ) ) ;
#11266=CIRCLE ( 'NONE', #3900, 6.050000000006050982 ) ;
#11270=CYLINDRICAL_SURFACE ( 'NONE', #440, 6.050000000006051870 ) ;
#11294=EDGE_CURVE ( 'NONE', #8124, #6155, #22304, .T. ) ;
#11295=LINE ( 'NONE', #4009, #12665 ) ;
#11297=EDGE_CURVE ( 'NONE', #21740, #1756, #21521, .T. ) ;
#11302=PRODUCT_DEFINITION_SHAPE ( 'NONE', 'NONE',  #8534 ) ;
#11311=ADVANCED_BREP_SHAPE_REPRESENTATION ( '', ( #2432, #8005 ), #18550 ) ;
#11324=DIRECTION ( 'NONE',  ( 1.000000000000000000, -0.000000000000000000, -0.000000000000000000 ) ) ;
#11341=CARTESIAN_POINT ( 'NONE',  ( 23.00000000000000000, 2.119223430970398336, -17.74893002550478016 ) ) ;
#11361=FACE_OUTER_BOUND ( 'NONE', #698, .T. ) ;
#11377=EDGE_LOOP ( 'NONE', ( #19917, #12388, #8414, #5260 ) ) ;
#11393=AXIS2_PLACEMENT_3D ( 'NONE', #567, #13236, #15440 ) ;
#11395=EDGE_LOOP ( 'NONE', ( #2020, #12151, #18478, #20016 ) ) ;
#11414=CARTESIAN_POINT ( 'NONE',  ( -10.00000000000000000, 0.000000000000000000, 0.000000000000000000 ) ) ;
#11421=DIRECTION ( 'NONE',  ( -1.000000000000000000, 0.000000000000000000, 0.000000000000000000 ) ) ;
#11427=DIRECTION ( 'NONE',  ( 0.000000000000000000, 0.000000000000000000, 1.000000000000000000 ) ) ;
#11431=DIRECTION ( 'NONE',  ( 0.000000000000000000, 0.9096319953545193293, -0.4154150130018842701 ) ) ;
#11442=EDGE_LOOP ( 'NONE', ( #14482, #8658, #9679, #5179 ) ) ;
#11445=CIRCLE ( 'NONE', #7945, 9.000000000000000000 ) ;
#11455=VERTEX_POINT ( 'NONE', #19288 ) ;
#11464=CARTESIAN_POINT ( 'NONE',  ( 0.000000000000000000, 0.000000000000000000, 0.000000000000000000 ) ) ;
#11469=ADVANCED_FACE ( 'NONE', ( #4170 ), #2572, .T. ) ;
#11479=AXIS2_PLACEMENT_3D ( 'NONE', #23936, #16247, #14291 ) ;
#11504=DIRECTION ( 'NONE',  ( -1.000000000000000000, 0.000000000000000000, -0.000000000000000000 ) ) ;
#11507=VECTOR ( 'NONE', #11504, 1000.000000000000000 ) ;
#11524=CARTESIAN_POINT ( 'NONE',  ( 23.00000000000000000, 8.890849273385601492, 7.584660931657517757 ) ) ;
#11533=FACE_OUTER_BOUND ( 'NONE', #5689, .T. ) ;
#11535=CARTESIAN_POINT ( 'NONE',  ( 23.00000000000000000, -9.239931321968246181, 10.79948145182496511 ) ) ;
#11537=LINE ( 'NONE', #15313, #4835 ) ;
#11544=ORIENTED_EDGE ( 'NONE', *, *, #14597, .T. ) ;
#11565=ORIENTED_EDGE ( 'NONE', *, *, #11294, .F. ) ;
#11597=AXIS2_PLACEMENT_3D ( 'NONE', #20581, #22536, #17140 ) ;
#11601=DIRECTION ( 'NONE',  ( -1.000000000000000000, 0.000000000000000000, 0.000000000000000000 ) ) ;
#11625=CIRCLE ( 'NONE', #14759, 17.87500000001787726 ) ;
#11642=VERTEX_POINT ( 'NONE', #12538 ) ;
#11653=ORIENTED_EDGE ( 'NONE', *, *, #16694, .F. ) ;
#11657=AXIS2_PLACEMENT_3D ( 'NONE', #9012, #9, #1591 ) ;
#11667=EDGE_LOOP ( 'NONE', ( #10448, #9238, #3194, #17909 ) ) ;
#11688=EDGE_CURVE ( 'NONE', #8545, #18646, #1228, .T. ) ;
#11696=CARTESIAN_POINT ( 'NONE',  ( 23.00000000000000000, 0.000000000000000000, 0.000000000000000000 ) ) ;
#11724=CARTESIAN_POINT ( 'NONE',  ( 23.00000000000000000, 0.000000000000000000, 0.000000000000000000 ) ) ;
#11727=CARTESIAN_POINT ( 'NONE',  ( -10.00000000000000000, 0.000000000000000000, 0.000000000000000000 ) ) ;
#11737=VERTEX_POINT ( 'NONE', #11179 ) ;
#11762=CARTESIAN_POINT ( 'NONE',  ( 23.00000000000000000, -6.393861490227802591, -9.782270569456514409 ) ) ;
#11781=CARTESIAN_POINT ( 'NONE',  ( 0.000000000000000000, 11.37860023611340665, 13.78561139983856521 ) ) ;
#11791=DIRECTION ( 'NONE',  ( -1.000000000000000000, -0.000000000000000000, -0.000000000000000000 ) ) ;
#11834=LINE ( 'NONE', #9745, #18807 ) ;
#11865=PRODUCT_DEFINITION_CONTEXT ( 'detailed design', #13382, 'design' ) ;
#11875=CIRCLE ( 'NONE', #2087, 11.68650000001168898 ) ;
#11889=CARTESIAN_POINT ( 'NONE',  ( 0.000000000000000000, 1.102182119232617714E-15, -9.000000000000000000 ) ) ;
#11892=CARTESIAN_POINT ( 'NONE',  ( 11.50000000000000000, 12.02595010061954461, 13.22467954916291433 ) ) ;
#11922=CARTESIAN_POINT ( 'NONE',  ( 23.00000000000000000, -13.61176534793449200, 10.13961790095610560 ) ) ;
#11940=DIRECTION ( 'NONE',  ( -1.000000000000000000, 0.000000000000000000, -0.000000000000000000 ) ) ;
#11945=DIRECTION ( 'NONE',  ( -1.000000000000000000, 0.000000000000000000, -0.000000000000000000 ) ) ;
#11946=DIRECTION ( 'NONE',  ( 0.000000000000000000, 0.000000000000000000, 1.000000000000000000 ) ) ;
#11968=ADVANCED_FACE ( 'NONE', ( #7764 ), #15922, .T. ) ;
#12003=CARTESIAN_POINT ( 'NONE',  ( 0.000000000000000000, -10.66755332433018744, -4.772587172891147311 ) ) ;
#12015=DIRECTION ( 'NONE',  ( -1.000000000000000000, 0.000000000000000000, 0.000000000000000000 ) ) ;
#12029=EDGE_CURVE ( 'NONE', #6200, #2336, #12560, .T. ) ;
#12034=DIRECTION ( 'NONE',  ( 0.000000000000000000, 0.000000000000000000, -1.000000000000000000 ) ) ;
#12041=VERTEX_POINT ( 'NONE', #4597 ) ;
#12044=ORIENTED_EDGE ( 'NONE', *, *, #23556, .F. ) ;
#12067=ORIENTED_EDGE ( 'NONE', *, *, #10422, .T. ) ;
#12070=DIRECTION ( 'NONE',  ( -1.000000000000000000, 0.000000000000000000, 0.000000000000000000 ) ) ;
#12088=ORIENTED_EDGE ( 'NONE', *, *, #3093, .F. ) ;
#12090=ORIENTED_EDGE ( 'NONE', *, *, #23900, .F. ) ;
#12112=CARTESIAN_POINT ( 'NONE',  ( 23.00000000000000000, -1.934484387512043435, 14.08058594723506474 ) ) ;
#12123=DIRECTION ( 'NONE',  ( -1.000000000000000000, 0.000000000000000000, -0.000000000000000000 ) ) ;
#12127=DIRECTION ( 'NONE',  ( 0.000000000000000000, 0.000000000000000000, 1.000000000000000000 ) ) ;
#12151=ORIENTED_EDGE ( 'NONE', *, *, #8641, .T. ) ;
#12164=AXIS2_PLACEMENT_3D ( 'NONE', #2824, #8906, #6857 ) ;
#12169=ORIENTED_EDGE ( 'NONE', *, *, #16694, .T. ) ;
#12170=VERTEX_POINT ( 'NONE', #3224 ) ;
#12174=EDGE_CURVE ( 'NONE', #21535, #19925, #13759, .T. ) ;
#12175=VERTEX_POINT ( 'NONE', #20553 ) ;
#12178=AXIS2_PLACEMENT_3D ( 'NONE', #3262, #8248, #15707 ) ;
#12197=CARTESIAN_POINT ( 'NONE',  ( 23.00000000000000000, 5.823083658124710738, 12.96521604808350503 ) ) ;
#12199=AXIS2_PLACEMENT_3D ( 'NONE', #9970, #15581, #15470 ) ;
#12203=VERTEX_POINT ( 'NONE', #18706 ) ;
#12210=DIRECTION ( 'NONE',  ( -1.000000000000000000, 0.000000000000000000, -0.000000000000000000 ) ) ;
#12226=ORIENTED_EDGE ( 'NONE', *, *, #6041, .F. ) ;
#12233=FACE_BOUND ( 'NONE', #2489, .T. ) ;
#12243=AXIS2_PLACEMENT_3D ( 'NONE', #20512, #1946, #9365 ) ;
#12253=DIRECTION ( 'NONE',  ( 0.000000000000000000, 0.000000000000000000, 1.000000000000000000 ) ) ;
#12256=EDGE_LOOP ( 'NONE', ( #10527, #19562, #9990, #20596 ) ) ;
#12258=DIRECTION ( 'NONE',  ( 0.000000000000000000, 0.5406408174555985546, -0.8412535328311806504 ) ) ;
#12273=ORIENTED_EDGE ( 'NONE', *, *, #23363, .F. ) ;
#12294=EDGE_CURVE ( 'NONE', #20664, #5794, #14534, .T. ) ;
#12297=CARTESIAN_POINT ( 'NONE',  ( -10.00000000000000000, 0.000000000000000000, 0.000000000000000000 ) ) ;
#12312=DIRECTION ( 'NONE',  ( -1.000000000000000000, 0.000000000000000000, 0.000000000000000000 ) ) ;
#12313=EDGE_CURVE ( 'NONE', #13157, #15534, #18958, .T. ) ;
#12325=CARTESIAN_POINT ( 'NONE',  ( 23.00000000000000000, 10.59264252385243665, -4.936618945406485714 ) ) ;
#12329=DIRECTION ( 'NONE',  ( 1.000000000000000000, 0.000000000000000000, 0.000000000000000000 ) ) ;
#12368=VERTEX_POINT ( 'NONE', #7713 ) ;
#12375=ADVANCED_FACE ( 'NONE', ( #18714 ), #19202, .T. ) ;
#12377=EDGE_LOOP ( 'NONE', ( #3849, #7850, #19692, #10495 ) ) ;
#12384=AXIS2_PLACEMENT_3D ( 'NONE', #17914, #14119, #21580 ) ;
#12388=ORIENTED_EDGE ( 'NONE', *, *, #6236, .F. ) ;
#12423=( NAMED_UNIT ( * ) PLANE_ANGLE_UNIT ( ) SI_UNIT ( $, .RADIAN. ) );
#12428=CYLINDRICAL_SURFACE ( 'NONE', #10350, 11.68650000001168721 ) ;
#12454=EDGE_CURVE ( 'NONE', #9276, #22027, #21582, .T. ) ;
#12462=AXIS2_PLACEMENT_3D ( 'NONE', #12197, #18073, #6723 ) ;
#12466=ADVANCED_FACE ( 'NONE', ( #9663 ), #17113, .T. ) ;
#12468=VERTEX_POINT ( 'NONE', #2356 ) ;
#12471=DIRECTION ( 'NONE',  ( -1.000000000000000000, -0.000000000000000000, 0.000000000000000000 ) ) ;
#12501=ORIENTED_EDGE ( 'NONE', *, *, #22034, .F. ) ;
#12518=DIRECTION ( 'NONE',  ( -1.000000000000000000, 0.000000000000000000, -0.000000000000000000 ) ) ;
#12538=CARTESIAN_POINT ( 'NONE',  ( 0.000000000000000000, -7.033831428820292331, 16.43291941292170577 ) ) ;
#12560=CIRCLE ( 'NONE', #13346, 17.87500000001787726 ) ;
#12564=DIRECTION ( 'NONE',  ( -1.000000000000000000, -0.000000000000000000, 0.000000000000000000 ) ) ;
#12565=CIRCLE ( 'NONE', #15686, 6.050000000006051870 ) ;
#12575=CARTESIAN_POINT ( 'NONE',  ( 23.00000000000000000, -6.393861490227931377, 9.782270569456429143 ) ) ;
#12622=DIRECTION ( 'NONE',  ( 0.000000000000000000, 0.7557495743542551603, 0.6548607339452887643 ) ) ;
#12627=ORIENTED_EDGE ( 'NONE', *, *, #22860, .F. ) ;
#12636=STYLED_ITEM('',(#24141),#2432);
#12638=CYLINDRICAL_SURFACE ( 'NONE', #3270, 6.050000000006050982 ) ;
#12664=CARTESIAN_POINT ( 'NONE',  ( 23.00000000000000000, -7.033831428820288778, 16.43291941292170577 ) ) ;
#12665=VECTOR ( 'NONE', #9477, 1000.000000000000000 ) ;
#12669=AXIS2_PLACEMENT_3D ( 'NONE', #3523, #23679, #10931 ) ;
#12689=VERTEX_POINT ( 'NONE', #3455 ) ;
#12714=DIRECTION ( 'NONE',  ( -1.000000000000000000, 0.000000000000000000, 0.000000000000000000 ) ) ;
#12746=LINE ( 'NONE', #18611, #11507 ) ;
#12765=VECTOR ( 'NONE', #19563, 1000.000000000000000 ) ;
#12801=CARTESIAN_POINT ( 'NONE',  ( 23.00000000000000000, 3.378881074890460745, -11.18737882312118082 ) ) ;
#12811=DIRECTION ( 'NONE',  ( 0.000000000000000000, 0.000000000000000000, 1.000000000000000000 ) ) ;
#12830=EDGE_CURVE ( 'NONE', #5794, #20973, #5645, .T. ) ;
#12840=DIRECTION ( 'NONE',  ( 1.000000000000000000, 0.000000000000000000, 0.000000000000000000 ) ) ;
#12849=CARTESIAN_POINT ( 'NONE',  ( 23.00000000000000000, 14.21257171757157245, 6.139082186136624486 ) ) ;
#12851=CIRCLE ( 'NONE', #15191, 17.87500000001787726 ) ;
#12867=AXIS2_PLACEMENT_3D ( 'NONE', #22968, #13811, #23673 ) ;
#12879=CARTESIAN_POINT ( 'NONE',  ( 23.00000000000000000, 6.242160243097161221, 9.879763041175145588 ) ) ;
#12899=CARTESIAN_POINT ( 'NONE',  ( 0.000000000000000000, 12.02595010061972403, -13.22467954916274913 ) ) ;
#12932=ORIENTED_EDGE ( 'NONE', *, *, #6879, .T. ) ;
#12941=CARTESIAN_POINT ( 'NONE',  ( 11.50000000000000000, -17.86986844953242937, 0.4282833139926494059 ) ) ;
#12958=ORIENTED_EDGE ( 'NONE', *, *, #16586, .F. ) ;
#12968=ORIENTED_EDGE ( 'NONE', *, *, #3791, .F. ) ;
#12987=PRODUCT_CONTEXT ( 'NONE', #9439, 'mechanical' ) ;
#12989=VERTEX_POINT ( 'NONE', #17707 ) ;
#12992=EDGE_CURVE ( 'NONE', #13157, #4844, #8777, .T. ) ;
#13003=ORIENTED_EDGE ( 'NONE', *, *, #1859, .T. ) ;
#13008=AXIS2_PLACEMENT_3D ( 'NONE', #23870, #1905, #22414 ) ;
#13050=CYLINDRICAL_SURFACE ( 'NONE', #12243, 11.68650000001168721 ) ;
#13053=CARTESIAN_POINT ( 'NONE',  ( 23.00000000000000000, 3.378881074890460745, -11.18737882312118082 ) ) ;
#13074=AXIS2_PLACEMENT_3D ( 'NONE', #6979, #2831, #17965 ) ;
#13075=FACE_OUTER_BOUND ( 'NONE', #13828, .T. ) ;
#13106=DIRECTION ( 'NONE',  ( 0.000000000000000000, 0.000000000000000000, -1.000000000000000000 ) ) ;
#13124=FACE_OUTER_BOUND ( 'NONE', #4378, .T. ) ;
#13131=DIRECTION ( 'NONE',  ( -1.000000000000000000, 0.000000000000000000, 0.000000000000000000 ) ) ;
#13132=LINE ( 'NONE', #334, #1366 ) ;
#13147=FACE_OUTER_BOUND ( 'NONE', #8783, .T. ) ;
#13148=CARTESIAN_POINT ( 'NONE',  ( 23.00000000000000000, 1.102182119232617714E-15, -9.000000000000000000 ) ) ;
#13157=VERTEX_POINT ( 'NONE', #16237 ) ;
#13172=DIRECTION ( 'NONE',  ( -1.000000000000000000, 0.000000000000000000, 0.000000000000000000 ) ) ;
#13194=ORIENTED_EDGE ( 'NONE', *, *, #10962, .F. ) ;
#13210=DIRECTION ( 'NONE',  ( 0.000000000000000000, 0.000000000000000000, 1.000000000000000000 ) ) ;
#13216=CARTESIAN_POINT ( 'NONE',  ( 11.50000000000000000, -14.80154252341788279, -10.02147513732838036 ) ) ;
#13219=EDGE_CURVE ( 'NONE', #20932, #12170, #22046, .T. ) ;
#13236=DIRECTION ( 'NONE',  ( 1.000000000000000000, 0.000000000000000000, 0.000000000000000000 ) ) ;
#13255=CARTESIAN_POINT ( 'NONE',  ( 0.000000000000000000, -7.812991839788663739, -16.07708877602020436 ) ) ;
#13271=ORIENTED_EDGE ( 'NONE', *, *, #993, .T. ) ;
#13289=EDGE_CURVE ( 'NONE', #11455, #15083, #21273, .T. ) ;
#13294=DIRECTION ( 'NONE',  ( -1.000000000000000000, -0.000000000000000000, 0.000000000000000000 ) ) ;
#13314=EDGE_CURVE ( 'NONE', #12468, #9726, #3842, .T. ) ;
#13328=VECTOR ( 'NONE', #6146, 1000.000000000000000 ) ;
#13346=AXIS2_PLACEMENT_3D ( 'NONE', #23134, #3885, #2177 ) ;
#13368=ORIENTED_EDGE ( 'NONE', *, *, #12830, .T. ) ;
#13382=APPLICATION_CONTEXT ( 'automotive_design' ) ;
#13412=DIRECTION ( 'NONE',  ( 1.000000000000000000, 0.000000000000000000, 0.000000000000000000 ) ) ;
#13421=EDGE_CURVE ( 'NONE', #8124, #9276, #12746, .T. ) ;
#13435=DIRECTION ( 'NONE',  ( 0.000000000000000000, 0.000000000000000000, 1.000000000000000000 ) ) ;
#13447=EDGE_CURVE ( 'NONE', #13479, #11063, #23234, .T. ) ;
#13473=CARTESIAN_POINT ( 'NONE',  ( 23.00000000000000000, 11.37860023611358962, -13.78561139983841421 ) ) ;
#13475=AXIS2_PLACEMENT_3D ( 'NONE', #23630, #20195, #22155 ) ;
#13477=ORIENTED_EDGE ( 'NONE', *, *, #10422, .F. ) ;
#13479=VERTEX_POINT ( 'NONE', #13473 ) ;
#13480=ADVANCED_FACE ( 'NONE', ( #15274 ), #20929, .T. ) ;
#13517=AXIS2_PLACEMENT_3D ( 'NONE', #1578, #1349, #19887 ) ;
#13521=DIRECTION ( 'NONE',  ( -1.000000000000000000, -0.000000000000000000, -0.000000000000000000 ) ) ;
#13528=CARTESIAN_POINT ( 'NONE',  ( 0.000000000000000000, 0.000000000000000000, 0.000000000000000000 ) ) ;
#13540=DIRECTION ( 'NONE',  ( -1.000000000000000000, 0.000000000000000000, 0.000000000000000000 ) ) ;
#13552=CARTESIAN_POINT ( 'NONE',  ( 11.50000000000000000, 2.119223430970397892, -17.74893002550478016 ) ) ;
#13563=DIRECTION ( 'NONE',  ( -1.000000000000000000, 0.000000000000000000, 0.000000000000000000 ) ) ;
#13566=ORIENTED_EDGE ( 'NONE', *, *, #13667, .F. ) ;
#13604=CARTESIAN_POINT ( 'NONE',  ( 23.00000000000000000, 12.00453763395396756, -1.558955687733494244 ) ) ;
#13607=CARTESIAN_POINT ( 'NONE',  ( 23.00000000000000000, -9.239931321968246181, 10.79948145182496511 ) ) ;
#13617=CARTESIAN_POINT ( 'NONE',  ( 23.00000000000000000, 12.00453763395396756, -7.608955687739546114 ) ) ;
#13626=ORIENTED_EDGE ( 'NONE', *, *, #23363, .T. ) ;
#13652=AXIS2_PLACEMENT_3D ( 'NONE', #15614, #23081, #8763 ) ;
#13657=LINE ( 'NONE', #8528, #16627 ) ;
#13667=EDGE_CURVE ( 'NONE', #14408, #8124, #20113, .T. ) ;
#13670=FACE_OUTER_BOUND ( 'NONE', #3958, .T. ) ;
#13682=CARTESIAN_POINT ( 'NONE',  ( 23.00000000000000000, -3.205857990849823480, 11.23818298448541420 ) ) ;
#13692=CARTESIAN_POINT ( 'NONE',  ( 0.000000000000000000, 11.58003564732003277, -1.573866785045813010 ) ) ;
#13721=CIRCLE ( 'NONE', #19181, 6.050000000006050982 ) ;
#13723=VERTEX_POINT ( 'NONE', #20405 ) ;
#13724=CARTESIAN_POINT ( 'NONE',  ( 0.000000000000000000, 12.00453763395396756, -7.608955687739546114 ) ) ;
#13732=LINE ( 'NONE', #11892, #2173 ) ;
#13734=VERTEX_POINT ( 'NONE', #2339 ) ;
#13743=CIRCLE ( 'NONE', #18433, 6.050000000006050982 ) ;
#13759=CIRCLE ( 'NONE', #16093, 6.050000000006052758 ) ;
#13775=EDGE_LOOP ( 'NONE', ( #21742, #1514, #11653, #6485 ) ) ;
#13776=AXIS2_PLACEMENT_3D ( 'NONE', #20888, #15369, #4177 ) ;
#13778=CARTESIAN_POINT ( 'NONE',  ( 0.000000000000000000, 0.000000000000000000, 0.000000000000000000 ) ) ;
#13797=DIRECTION ( 'NONE',  ( 1.000000000000000000, 0.000000000000000000, 0.000000000000000000 ) ) ;
#13811=DIRECTION ( 'NONE',  ( -1.000000000000000000, -0.000000000000000000, -0.000000000000000000 ) ) ;
#13828=EDGE_LOOP ( 'NONE', ( #19972, #10736, #13925, #23104 ) ) ;
#13856=ORIENTED_EDGE ( 'NONE', *, *, #17516, .F. ) ;
#13870=DIRECTION ( 'NONE',  ( 0.000000000000000000, 0.000000000000000000, 1.000000000000000000 ) ) ;
#13879=ORIENTED_EDGE ( 'NONE', *, *, #16817, .T. ) ;
#13881=ADVANCED_FACE ( 'NONE', ( #22083 ), #19776, .F. ) ;
#13888=LINE ( 'NONE', #8006, #10080 ) ;
#13891=CARTESIAN_POINT ( 'NONE',  ( 23.00000000000000000, 17.26667456984545979, 4.623588898214379128 ) ) ;
#13896=CARTESIAN_POINT ( 'NONE',  ( 23.00000000000000000, 0.000000000000000000, 0.000000000000000000 ) ) ;
#13925=ORIENTED_EDGE ( 'NONE', *, *, #18409, .T. ) ;
#13998=EDGE_LOOP ( 'NONE', ( #13856, #16786, #15846, #18989 ) ) ;
#14011=DIRECTION ( 'NONE',  ( -1.000000000000000000, 0.000000000000000000, -0.000000000000000000 ) ) ;
#14042=DIRECTION ( 'NONE',  ( 1.000000000000000000, 0.000000000000000000, 0.000000000000000000 ) ) ;
#14119=DIRECTION ( 'NONE',  ( -1.000000000000000000, -0.000000000000000000, 0.000000000000000000 ) ) ;
#14155=AXIS2_PLACEMENT_3D ( 'NONE', #23631, #12123, #12258 ) ;
#14162=ORIENTED_EDGE ( 'NONE', *, *, #20076, .T. ) ;
#14174=CARTESIAN_POINT ( 'NONE',  ( 23.00000000000000000, 5.985147671565707483, 12.89120389306417103 ) ) ;
#14177=CIRCLE ( 'NONE', #1327, 6.050000000006053646 ) ;
#14179=AXIS2_PLACEMENT_3D ( 'NONE', #8127, #15570, #23033 ) ;
#14208=EDGE_CURVE ( 'NONE', #19925, #19205, #13657, .T. ) ;
#14214=AXIS2_PLACEMENT_3D ( 'NONE', #18446, #9162, #16610 ) ;
#14238=AXIS2_PLACEMENT_3D ( 'NONE', #15546, #23012, #6287 ) ;
#14250=EDGE_LOOP ( 'NONE', ( #9007, #7835, #7698, #9259 ) ) ;
#14252=EDGE_CURVE ( 'NONE', #11063, #21535, #17002, .T. ) ;
#14268=DIRECTION ( 'NONE',  ( -1.000000000000000000, 0.000000000000000000, 0.000000000000000000 ) ) ;
#14274=CIRCLE ( 'NONE', #18194, 17.87500000001787726 ) ;
#14291=DIRECTION ( 'NONE',  ( 0.000000000000000000, 0.000000000000000000, 1.000000000000000000 ) ) ;
#14316=DIRECTION ( 'NONE',  ( -1.000000000000000000, 0.000000000000000000, -0.000000000000000000 ) ) ;
#14327=ADVANCED_FACE ( 'NONE', ( #3285 ), #7297, .T. ) ;
#14356=ORIENTED_EDGE ( 'NONE', *, *, #22418, .T. ) ;
#14357=LINE ( 'NONE', #3503, #3199 ) ;
#14372=ORIENTED_EDGE ( 'NONE', *, *, #19934, .T. ) ;
#14384=ORIENTED_EDGE ( 'NONE', *, *, #20335, .T. ) ;
#14387=CARTESIAN_POINT ( 'NONE',  ( 0.000000000000000000, 0.000000000000000000, 0.000000000000000000 ) ) ;
#14396=CIRCLE ( 'NONE', #20265, 11.68650000001168721 ) ;
#14408=VERTEX_POINT ( 'NONE', #23396 ) ;
#14433=CARTESIAN_POINT ( 'NONE',  ( 11.50000000000000000, -15.26463740537719005, -9.300885435430258141 ) ) ;
#14435=CARTESIAN_POINT ( 'NONE',  ( 23.00000000000000000, -9.374578970469563899, -10.68280860024325030 ) ) ;
#14436=AXIS2_PLACEMENT_3D ( 'NONE', #2892, #8114, #4613 ) ;
#14459=DIRECTION ( 'NONE',  ( 0.000000000000000000, 0.9898214418809322401, 0.1423148382732887240 ) ) ;
#14482=ORIENTED_EDGE ( 'NONE', *, *, #21940, .T. ) ;
#14510=ADVANCED_FACE ( 'NONE', ( #11132 ), #5186, .T. ) ;
#14521=AXIS2_PLACEMENT_3D ( 'NONE', #14435, #17890, #8949 ) ;
#14532=CIRCLE ( 'NONE', #4020, 17.87500000001787726 ) ;
#14534=CIRCLE ( 'NONE', #20378, 6.050000000006050982 ) ;
#14597=EDGE_CURVE ( 'NONE', #23003, #4197, #19734, .T. ) ;
#14600=FACE_OUTER_BOUND ( 'NONE', #16132, .T. ) ;
#14603=EDGE_CURVE ( 'NONE', #4837, #12368, #13732, .T. ) ;
#14607=ADVANCED_FACE ( 'NONE', ( #10660 ), #2752, .T. ) ;
#14643=AXIS2_PLACEMENT_3D ( 'NONE', #17374, #8081, #22994 ) ;
#14650=DIRECTION ( 'NONE',  ( -1.000000000000000000, -0.000000000000000000, -0.000000000000000000 ) ) ;
#14698=DIRECTION ( 'NONE',  ( -1.000000000000000000, 0.000000000000000000, -0.000000000000000000 ) ) ;
#14710=VERTEX_POINT ( 'NONE', #4717 ) ;
#14718=EDGE_CURVE ( 'NONE', #23514, #14903, #7240, .T. ) ;
#14730=CARTESIAN_POINT ( 'NONE',  ( 0.000000000000000000, 0.000000000000000000, 0.000000000000000000 ) ) ;
#14732=ORIENTED_EDGE ( 'NONE', *, *, #3791, .T. ) ;
#14741=FACE_OUTER_BOUND ( 'NONE', #17239, .T. ) ;
#14759=AXIS2_PLACEMENT_3D ( 'NONE', #5997, #157, #13435 ) ;
#14769=EDGE_CURVE ( 'NONE', #2336, #20664, #23843, .T. ) ;
#14809=ORIENTED_EDGE ( 'NONE', *, *, #4635, .T. ) ;
#14813=EDGE_LOOP ( 'NONE', ( #12067, #15858, #21640, #10642 ) ) ;
#14846=CARTESIAN_POINT ( 'NONE',  ( 0.000000000000000000, 17.02535186363812514, -5.445458559198937287 ) ) ;
#14879=DIRECTION ( 'NONE',  ( 0.000000000000000000, 0.000000000000000000, 1.000000000000000000 ) ) ;
#14896=ADVANCED_FACE ( 'NONE', ( #1927 ), #5362, .T. ) ;
#14903=VERTEX_POINT ( 'NONE', #22200 ) ;
#14939=LINE ( 'NONE', #16895, #16977 ) ;
#14940=CARTESIAN_POINT ( 'NONE',  ( 0.000000000000000000, -13.66196005206961850, -3.918670437617226110 ) ) ;
#14942=CARTESIAN_POINT ( 'NONE',  ( 0.000000000000000000, -13.61176534793449200, 10.13961790095610560 ) ) ;
#14943=ORIENTED_EDGE ( 'NONE', *, *, #23900, .T. ) ;
#14959=ORIENTED_EDGE ( 'NONE', *, *, #23643, .F. ) ;
#14967=AXIS2_PLACEMENT_3D ( 'NONE', #4601, #4227, #4346 ) ;
#14984=VERTEX_POINT ( 'NONE', #13891 ) ;
#14988=VECTOR ( 'NONE', #17848, 1000.000000000000000 ) ;
#15010=CARTESIAN_POINT ( 'NONE',  ( 23.00000000000000000, 12.00453763395397466, 7.608955687739546114 ) ) ;
#15014=FACE_OUTER_BOUND ( 'NONE', #23111, .T. ) ;
#15024=AXIS2_PLACEMENT_3D ( 'NONE', #15976, #23436, #17940 ) ;
#15028=CARTESIAN_POINT ( 'NONE',  ( 0.000000000000000000, -9.239931321968246181, 10.79948145182496511 ) ) ;
#15031=ORIENTED_EDGE ( 'NONE', *, *, #23948, .T. ) ;
#15033=AXIS2_PLACEMENT_3D ( 'NONE', #3817, #11224, #1968 ) ;
#15058=CARTESIAN_POINT ( 'NONE',  ( 23.00000000000000000, 11.58003564732003277, -1.573866785045813010 ) ) ;
#15062=DIRECTION ( 'NONE',  ( -1.000000000000000000, 0.000000000000000000, 0.000000000000000000 ) ) ;
#15080=AXIS2_PLACEMENT_3D ( 'NONE', #2236, #9658, #2480 ) ;
#15083=VERTEX_POINT ( 'NONE', #4867 ) ;
#15119=DIRECTION ( 'NONE',  ( 0.000000000000000000, -0.2817325568414366654, 0.9594929736144953702 ) ) ;
#15121=CARTESIAN_POINT ( 'NONE',  ( 0.000000000000000000, -2.110835303355385051, 14.05523051341064722 ) ) ;
#15146=ORIENTED_EDGE ( 'NONE', *, *, #6533, .T. ) ;
#15151=ORIENTED_EDGE ( 'NONE', *, *, #9515, .T. ) ;
#15152=CYLINDRICAL_SURFACE ( 'NONE', #8321, 6.050000000006050982 ) ;
#15154=DIRECTION ( 'NONE',  ( 0.000000000000000000, -0.9096319953545136672, -0.4154150130018965936 ) ) ;
#15170=CARTESIAN_POINT ( 'NONE',  ( 23.00000000000000000, 3.378881074890309311, 11.18737882312122878 ) ) ;
#15191=AXIS2_PLACEMENT_3D ( 'NONE', #14730, #11047, #21944 ) ;
#15192=EDGE_LOOP ( 'NONE', ( #9237, #1900, #15146, #12090 ) ) ;
#15203=CARTESIAN_POINT ( 'NONE',  ( 23.00000000000000000, 0.000000000000000000, 0.000000000000000000 ) ) ;
#15212=EDGE_LOOP ( 'NONE', ( #6401, #6561, #4961, #6985 ) ) ;
#15233=DIRECTION ( 'NONE',  ( -1.000000000000000000, -0.000000000000000000, -0.000000000000000000 ) ) ;
#15242=VECTOR ( 'NONE', #18276, 1000.000000000000000 ) ;
#15261=VERTEX_POINT ( 'NONE', #15058 ) ;
#15269=CARTESIAN_POINT ( 'NONE',  ( -10.00000000000000000, 0.000000000000000000, 0.000000000000000000 ) ) ;
#15271=ORIENTED_EDGE ( 'NONE', *, *, #12313, .T. ) ;
#15274=FACE_OUTER_BOUND ( 'NONE', #15942, .T. ) ;
#15283=AXIS2_PLACEMENT_3D ( 'NONE', #11464, #19169, #18939 ) ;
#15313=CARTESIAN_POINT ( 'NONE',  ( 23.00000000000000000, 8.890849273385601492, 7.584660931657517757 ) ) ;
#15318=ORIENTED_EDGE ( 'NONE', *, *, #16256, .F. ) ;
#15320=VERTEX_POINT ( 'NONE', #17388 ) ;
#15344=( GEOMETRIC_REPRESENTATION_CONTEXT ( 3 ) GLOBAL_UNCERTAINTY_ASSIGNED_CONTEXT ( ( #7872 ) ) GLOBAL_UNIT_ASSIGNED_CONTEXT ( ( #3623, #7039, #3272 ) ) REPRESENTATION_CONTEXT ( 'NONE', 'WORKASPACE' ) );
#15369=DIRECTION ( 'NONE',  ( -1.000000000000000000, -0.000000000000000000, -0.000000000000000000 ) ) ;
#15387=AXIS2_PLACEMENT_3D ( 'NONE', #175, #12840, #16856 ) ;
#15398=VERTEX_POINT ( 'NONE', #19223 ) ;
#15440=DIRECTION ( 'NONE',  ( 0.000000000000000000, 0.000000000000000000, -1.000000000000000000 ) ) ;
#15470=DIRECTION ( 'NONE',  ( 0.000000000000000000, -0.9898214418809341275, 0.1423148382732755957 ) ) ;
#15484=DIRECTION ( 'NONE',  ( 1.000000000000000000, 0.000000000000000000, 0.000000000000000000 ) ) ;
#15534=VERTEX_POINT ( 'NONE', #10042 ) ;
#15544=DIRECTION ( 'NONE',  ( -1.000000000000000000, 0.000000000000000000, 0.000000000000000000 ) ) ;
#15546=CARTESIAN_POINT ( 'NONE',  ( 0.000000000000000000, 0.000000000000000000, 0.000000000000000000 ) ) ;
#15552=EDGE_CURVE ( 'NONE', #14710, #9146, #23106, .T. ) ;
#15570=DIRECTION ( 'NONE',  ( -1.000000000000000000, -0.000000000000000000, -0.000000000000000000 ) ) ;
#15581=DIRECTION ( 'NONE',  ( -1.000000000000000000, 0.000000000000000000, 0.000000000000000000 ) ) ;
#15613=ORIENTED_EDGE ( 'NONE', *, *, #8492, .F. ) ;
#15614=CARTESIAN_POINT ( 'NONE',  ( 23.00000000000000000, 0.000000000000000000, 0.000000000000000000 ) ) ;
#15616=CARTESIAN_POINT ( 'NONE',  ( 23.00000000000000000, 0.000000000000000000, 0.000000000000000000 ) ) ;
#15657=CARTESIAN_POINT ( 'NONE',  ( 0.000000000000000000, 5.823083658124882156, -12.96521604808343398 ) ) ;
#15684=ORIENTED_EDGE ( 'NONE', *, *, #11688, .T. ) ;
#15686=AXIS2_PLACEMENT_3D ( 'NONE', #17434, #6330, #8029 ) ;
#15695=DIRECTION ( 'NONE',  ( 0.000000000000000000, 0.000000000000000000, 1.000000000000000000 ) ) ;
#15707=DIRECTION ( 'NONE',  ( 0.000000000000000000, 0.000000000000000000, 1.000000000000000000 ) ) ;
#15709=CARTESIAN_POINT ( 'NONE',  ( 23.00000000000000000, 0.000000000000000000, 0.000000000000000000 ) ) ;
#15732=DIRECTION ( 'NONE',  ( -1.000000000000000000, 0.000000000000000000, 0.000000000000000000 ) ) ;
#15738=ORIENTED_EDGE ( 'NONE', *, *, #16902, .F. ) ;
#15745=AXIS2_PLACEMENT_3D ( 'NONE', #17342, #12070, #19543 ) ;
#15779=CARTESIAN_POINT ( 'NONE',  ( 23.00000000000000000, 0.000000000000000000, 0.000000000000000000 ) ) ;
#15783=ORIENTED_EDGE ( 'NONE', *, *, #16256, .T. ) ;
#15788=CIRCLE ( 'NONE', #15387, 6.050000000006050982 ) ;
#15792=ORIENTED_EDGE ( 'NONE', *, *, #22529, .F. ) ;
#15821=VERTEX_POINT ( 'NONE', #18406 ) ;
#15842=CARTESIAN_POINT ( 'NONE',  ( 23.00000000000000000, -1.934484387511856252, -14.08058594723508072 ) ) ;
#15846=ORIENTED_EDGE ( 'NONE', *, *, #11294, .T. ) ;
#15856=ADVANCED_FACE ( 'NONE', ( #14741 ), #22204, .T. ) ;
#15858=ORIENTED_EDGE ( 'NONE', *, *, #7590, .F. ) ;
#15863=DIRECTION ( 'NONE',  ( 0.000000000000000000, 0.000000000000000000, -1.000000000000000000 ) ) ;
#15873=LINE ( 'NONE', #19533, #18753 ) ;
#15874=PLANE ( 'NONE',  #9850 ) ;
#15892=ORIENTED_EDGE ( 'NONE', *, *, #9208, .T. ) ;
#15904=ORIENTED_EDGE ( 'NONE', *, *, #6046, .T. ) ;
#15922=CYLINDRICAL_SURFACE ( 'NONE', #21140, 6.050000000006050982 ) ;
#15924=DIRECTION ( 'NONE',  ( -1.000000000000000000, 0.000000000000000000, -0.000000000000000000 ) ) ;
#15936=AXIS2_PLACEMENT_3D ( 'NONE', #15121, #4418, #18938 ) ;
#15942=EDGE_LOOP ( 'NONE', ( #21017, #6350, #1740, #15151 ) ) ;
#15976=CARTESIAN_POINT ( 'NONE',  ( 23.00000000000000000, -2.110835303355385051, 14.05523051341064722 ) ) ;
#15999=VECTOR ( 'NONE', #12015, 1000.000000000000000 ) ;
#16008=VERTEX_POINT ( 'NONE', #11781 ) ;
#16013=CARTESIAN_POINT ( 'NONE',  ( 0.000000000000000000, -14.80154252341788279, -10.02147513732838036 ) ) ;
#16041=CARTESIAN_POINT ( 'NONE',  ( -10.00000000000000000, 0.000000000000000000, 0.000000000000000000 ) ) ;
#16042=DIRECTION ( 'NONE',  ( 1.000000000000000000, 0.000000000000000000, 0.000000000000000000 ) ) ;
#16053=PRODUCT ( 'spur gear_am_Metric - Spur gear 2.75M 11T 20PA 23FW ---S11N75H50L18N', 'spur gear_am_Metric - Spur gear 2.75M 11T 20PA 23FW ---S11N75H50L18N', '', ( #12987 ) ) ;
#16062=CARTESIAN_POINT ( 'NONE',  ( 0.000000000000000000, 5.823083658124710738, 12.96521604808350503 ) ) ;
#16074=CARTESIAN_POINT ( 'NONE',  ( 0.000000000000000000, -7.812991839788872461, 16.07708877602009068 ) ) ;
#16089=ADVANCED_FACE ( 'NONE', ( #2292 ), #717, .T. ) ;
#16093=AXIS2_PLACEMENT_3D ( 'NONE', #16273, #23734, #7001 ) ;
#16109=AXIS2_PLACEMENT_3D ( 'NONE', #635, #4660, #6114 ) ;
#16116=AXIS2_PLACEMENT_3D ( 'NONE', #23733, #7000, #19836 ) ;
#16126=EDGE_CURVE ( 'NONE', #10574, #14984, #19660, .T. ) ;
#16132=EDGE_LOOP ( 'NONE', ( #10296, #15904, #12501, #3 ) ) ;
#16168=AXIS2_PLACEMENT_3D ( 'NONE', #4538, #11945, #19411 ) ;
#16173=AXIS2_PLACEMENT_3D ( 'NONE', #8015, #13172, #20629 ) ;
#16232=FACE_BOUND ( 'NONE', #2922, .T. ) ;
#16236=LINE ( 'NONE', #21846, #5457 ) ;
#16237=CARTESIAN_POINT ( 'NONE',  ( 23.00000000000000000, 10.59264252385236738, 4.936618945406631376 ) ) ;
#16247=DIRECTION ( 'NONE',  ( -1.000000000000000000, -0.000000000000000000, 0.000000000000000000 ) ) ;
#16256=EDGE_CURVE ( 'NONE', #18301, #12468, #2090, .T. ) ;
#16257=CARTESIAN_POINT ( 'NONE',  ( 11.50000000000000000, 17.02535186363812514, -5.445458559198938175 ) ) ;
#16273=CARTESIAN_POINT ( 'NONE',  ( 23.00000000000000000, -1.934484387511856252, -14.08058594723508072 ) ) ;
#16276=DIRECTION ( 'NONE',  ( -1.000000000000000000, 0.000000000000000000, 0.000000000000000000 ) ) ;
#16282=ADVANCED_FACE ( 'NONE', ( #10907 ), #12638, .T. ) ;
#16324=ORIENTED_EDGE ( 'NONE', *, *, #5021, .T. ) ;
#16336=EDGE_CURVE ( 'NONE', #4197, #11455, #5220, .T. ) ;
#16383=ORIENTED_EDGE ( 'NONE', *, *, #22034, .T. ) ;
#16384=DIRECTION ( 'NONE',  ( -1.000000000000000000, 0.000000000000000000, 0.000000000000000000 ) ) ;
#16395=AXIS2_PLACEMENT_3D ( 'NONE', #16908, #1563, #16420 ) ;
#16412=AXIS2_PLACEMENT_3D ( 'NONE', #6145, #21030, #18712 ) ;
#16420=DIRECTION ( 'NONE',  ( 0.000000000000000000, -0.7557495743542638200, 0.6548607339452786613 ) ) ;
#16421=DIRECTION ( 'NONE',  ( 0.000000000000000000, 0.000000000000000000, 1.000000000000000000 ) ) ;
#16440=VECTOR ( 'NONE', #21707, 1000.000000000000000 ) ;
#16468=DIRECTION ( 'NONE',  ( 0.000000000000000000, -0.7557495743542637090, 0.6548607339452788834 ) ) ;
#16475=CYLINDRICAL_SURFACE ( 'NONE', #11479, 6.050000000006051870 ) ;
#16499=DIRECTION ( 'NONE',  ( -1.000000000000000000, 0.000000000000000000, 0.000000000000000000 ) ) ;
#16503=ADVANCED_FACE ( 'NONE', ( #21668 ), #3004, .T. ) ;
#16507=ORIENTED_EDGE ( 'NONE', *, *, #18701, .F. ) ;
#16511=AXIS2_PLACEMENT_3D ( 'NONE', #5076, #18006, #12622 ) ;
#16531=ORIENTED_EDGE ( 'NONE', *, *, #23461, .F. ) ;
#16554=CIRCLE ( 'NONE', #9153, 6.050000000006050982 ) ;
#16570=DIRECTION ( 'NONE',  ( 0.000000000000000000, 0.000000000000000000, 1.000000000000000000 ) ) ;
#16586=EDGE_CURVE ( 'NONE', #9726, #6008, #23575, .T. ) ;
#16610=DIRECTION ( 'NONE',  ( 0.000000000000000000, 0.7557495743542551603, 0.6548607339452887643 ) ) ;
#16611=CARTESIAN_POINT ( 'NONE',  ( 0.000000000000000000, -6.393861490227802591, -9.782270569456514409 ) ) ;
#16627=VECTOR ( 'NONE', #11940, 1000.000000000000000 ) ;
#16632=AXIS2_PLACEMENT_3D ( 'NONE', #10534, #16276, #17996 ) ;
#16640=VERTEX_POINT ( 'NONE', #2835 ) ;
#16650=DIRECTION ( 'NONE',  ( -1.000000000000000000, -0.000000000000000000, 0.000000000000000000 ) ) ;
#16694=EDGE_CURVE ( 'NONE', #3225, #19080, #10859, .T. ) ;
#16695=DIRECTION ( 'NONE',  ( -1.000000000000000000, -0.000000000000000000, 0.000000000000000000 ) ) ;
#16739=ORIENTED_EDGE ( 'NONE', *, *, #23780, .T. ) ;
#16742=DIRECTION ( 'NONE',  ( -1.000000000000000000, 0.000000000000000000, 0.000000000000000000 ) ) ;
#16774=LINE ( 'NONE', #18270, #3617 ) ;
#16783=CARTESIAN_POINT ( 'NONE',  ( 23.00000000000000000, -0.09016380984455869829, -11.68615217844040721 ) ) ;
#16786=ORIENTED_EDGE ( 'NONE', *, *, #13421, .F. ) ;
#16817=EDGE_CURVE ( 'NONE', #23927, #20733, #7198, .T. ) ;
#16849=ADVANCED_FACE ( 'NONE', ( #22354 ), #832, .T. ) ;
#16856=DIRECTION ( 'NONE',  ( 0.000000000000000000, 0.000000000000000000, -1.000000000000000000 ) ) ;
#16895=CARTESIAN_POINT ( 'NONE',  ( 23.00000000000000000, -13.66196005206961850, 2.131329562388824428 ) ) ;
#16902=EDGE_CURVE ( 'NONE', #8545, #23927, #592, .T. ) ;
#16908=CARTESIAN_POINT ( 'NONE',  ( 0.000000000000000000, -13.61176534793443338, -4.089617900950226925 ) ) ;
#16912=VECTOR ( 'NONE', #19645, 1000.000000000000000 ) ;
#16930=DIRECTION ( 'NONE',  ( 0.000000000000000000, 0.000000000000000000, 1.000000000000000000 ) ) ;
#16937=CYLINDRICAL_SURFACE ( 'NONE', #17615, 17.87500000001787726 ) ;
#16966=AXIS2_PLACEMENT_3D ( 'NONE', #422, #7720, #15154 ) ;
#16977=VECTOR ( 'NONE', #22415, 1000.000000000000000 ) ;
#16981=ORIENTED_EDGE ( 'NONE', *, *, #3093, .T. ) ;
#17002=CIRCLE ( 'NONE', #13517, 11.68650000001168721 ) ;
#17026=CARTESIAN_POINT ( 'NONE',  ( 23.00000000000000000, 12.00453763395396756, -7.608955687739546114 ) ) ;
#17062=CIRCLE ( 'NONE', #17077, 6.050000000006050982 ) ;
#17064=LINE ( 'NONE', #4018, #4084 ) ;
#17077=AXIS2_PLACEMENT_3D ( 'NONE', #4044, #13294, #2214 ) ;
#17095=ADVANCED_FACE ( 'NONE', ( #20837 ), #576, .T. ) ;
#17113=CYLINDRICAL_SURFACE ( 'NONE', #19238, 17.87500000001787726 ) ;
#17129=ORIENTED_EDGE ( 'NONE', *, *, #22418, .F. ) ;
#17140=DIRECTION ( 'NONE',  ( 0.000000000000000000, 0.000000000000000000, 1.000000000000000000 ) ) ;
#17184=DIRECTION ( 'NONE',  ( -1.000000000000000000, 0.000000000000000000, 0.000000000000000000 ) ) ;
#17201=DIRECTION ( 'NONE',  ( 1.000000000000000000, 0.000000000000000000, 0.000000000000000000 ) ) ;
#17215=AXIS2_PLACEMENT_3D ( 'NONE', #6222, #9866, #11946 ) ;
#17239=EDGE_LOOP ( 'NONE', ( #2371, #12958, #10611, #16739 ) ) ;
#17270=FACE_OUTER_BOUND ( 'NONE', #9529, .T. ) ;
#17278=EDGE_CURVE ( 'NONE', #4776, #3225, #2888, .T. ) ;
#17292=DIRECTION ( 'NONE',  ( 1.000000000000000000, 0.000000000000000000, 0.000000000000000000 ) ) ;
#17311=EDGE_LOOP ( 'NONE', ( #1034, #18743, #20100, #4984 ) ) ;
#17325=ORIENTED_EDGE ( 'NONE', *, *, #23461, .T. ) ;
#17337=FACE_OUTER_BOUND ( 'NONE', #4566, .T. ) ;
#17342=CARTESIAN_POINT ( 'NONE',  ( 23.00000000000000000, 0.000000000000000000, 0.000000000000000000 ) ) ;
#17360=EDGE_CURVE ( 'NONE', #20283, #15320, #20806, .T. ) ;
#17364=ORIENTED_EDGE ( 'NONE', *, *, #14718, .F. ) ;
#17374=CARTESIAN_POINT ( 'NONE',  ( 23.00000000000000000, 0.000000000000000000, 0.000000000000000000 ) ) ;
#17388=CARTESIAN_POINT ( 'NONE',  ( 23.00000000000000000, -17.86986844953242226, -0.4282833139928861610 ) ) ;
#17399=ORIENTED_EDGE ( 'NONE', *, *, #18153, .F. ) ;
#17421=CARTESIAN_POINT ( 'NONE',  ( 0.000000000000000000, 0.000000000000000000, 0.000000000000000000 ) ) ;
#17425=DIRECTION ( 'NONE',  ( 0.000000000000000000, 0.000000000000000000, 1.000000000000000000 ) ) ;
#17434=CARTESIAN_POINT ( 'NONE',  ( 23.00000000000000000, -9.374578970469700678, 10.68280860024311885 ) ) ;
#17480=DIRECTION ( 'NONE',  ( -1.000000000000000000, 0.000000000000000000, 0.000000000000000000 ) ) ;
#17486=CARTESIAN_POINT ( 'NONE',  ( 0.000000000000000000, -13.61176534793449200, 4.089617900950054619 ) ) ;
#17489=ORIENTED_EDGE ( 'NONE', *, *, #5311, .F. ) ;
#17503=DIRECTION ( 'NONE',  ( -1.000000000000000000, 0.000000000000000000, 0.000000000000000000 ) ) ;
#17505=VECTOR ( 'NONE', #15544, 1000.000000000000000 ) ;
#17508=CARTESIAN_POINT ( 'NONE',  ( 0.000000000000000000, -3.205857990849673378, -11.23818298448545860 ) ) ;
#17512=EDGE_CURVE ( 'NONE', #7020, #6200, #20431, .T. ) ;
#17515=ORIENTED_EDGE ( 'NONE', *, *, #4635, .F. ) ;
#17516=EDGE_CURVE ( 'NONE', #9276, #3367, #11875, .T. ) ;
#17519=ORIENTED_EDGE ( 'NONE', *, *, #1859, .F. ) ;
#17523=ADVANCED_FACE ( 'NONE', ( #11361 ), #15152, .T. ) ;
#17526=DIRECTION ( 'NONE',  ( 1.000000000000000000, -0.000000000000000000, -0.000000000000000000 ) ) ;
#17552=CYLINDRICAL_SURFACE ( 'NONE', #23942, 6.050000000006051870 ) ;
#17581=VECTOR ( 'NONE', #22294, 1000.000000000000000 ) ;
#17610=ORIENTED_EDGE ( 'NONE', *, *, #2156, .F. ) ;
#17615=AXIS2_PLACEMENT_3D ( 'NONE', #7530, #10944, #20368 ) ;
#17620=ORIENTED_EDGE ( 'NONE', *, *, #19932, .F. ) ;
#17656=AXIS2_PLACEMENT_3D ( 'NONE', #20465, #13131, #3866 ) ;
#17660=EDGE_CURVE ( 'NONE', #3712, #7231, #8726, .T. ) ;
#17671=DIRECTION ( 'NONE',  ( 1.000000000000000000, -0.000000000000000000, -0.000000000000000000 ) ) ;
#17707=CARTESIAN_POINT ( 'NONE',  ( 0.000000000000000000, 14.21257171757157245, 6.139082186136624486 ) ) ;
#17708=ORIENTED_EDGE ( 'NONE', *, *, #18380, .F. ) ;
#17819=EDGE_CURVE ( 'NONE', #7640, #8629, #1158, .T. ) ;
#17826=CIRCLE ( 'NONE', #10348, 6.050000000006050982 ) ;
#17848=DIRECTION ( 'NONE',  ( -1.000000000000000000, -0.000000000000000000, 0.000000000000000000 ) ) ;
#17887=DIRECTION ( 'NONE',  ( 0.000000000000000000, 0.000000000000000000, 1.000000000000000000 ) ) ;
#17890=DIRECTION ( 'NONE',  ( -1.000000000000000000, -0.000000000000000000, 0.000000000000000000 ) ) ;
#17901=CARTESIAN_POINT ( 'NONE',  ( 23.00000000000000000, 11.58003564732003277, 1.573866785045813899 ) ) ;
#17909=ORIENTED_EDGE ( 'NONE', *, *, #15552, .T. ) ;
#17912=CARTESIAN_POINT ( 'NONE',  ( 23.00000000000000000, 0.000000000000000000, 0.000000000000000000 ) ) ;
#17914=CARTESIAN_POINT ( 'NONE',  ( 23.00000000000000000, 5.823083658124882156, -12.96521604808343398 ) ) ;
#17918=CARTESIAN_POINT ( 'NONE',  ( 0.000000000000000000, 0.000000000000000000, 0.000000000000000000 ) ) ;
#17924=CARTESIAN_POINT ( 'NONE',  ( 50.00005079999999680, 1.102182119232617714E-15, -9.000000000000000000 ) ) ;
#17933=CARTESIAN_POINT ( 'NONE',  ( 50.00005079999999680, 0.000000000000000000, 0.000000000000000000 ) ) ;
#17937=VECTOR ( 'NONE', #23449, 1000.000000000000000 ) ;
#17940=DIRECTION ( 'NONE',  ( 0.000000000000000000, 0.000000000000000000, 1.000000000000000000 ) ) ;
#17953=ADVANCED_FACE ( 'NONE', ( #15014 ), #11107, .T. ) ;
#17965=DIRECTION ( 'NONE',  ( 0.000000000000000000, 0.9096319953545193293, -0.4154150130018842701 ) ) ;
#17996=DIRECTION ( 'NONE',  ( 0.000000000000000000, -0.2817325568414367765, 0.9594929736144953702 ) ) ;
#18002=CYLINDRICAL_SURFACE ( 'NONE', #19867, 17.87500000001787726 ) ;
#18006=DIRECTION ( 'NONE',  ( -1.000000000000000000, 0.000000000000000000, 0.000000000000000000 ) ) ;
#18023=DIRECTION ( 'NONE',  ( -1.000000000000000000, 0.000000000000000000, 0.000000000000000000 ) ) ;
#18038=VECTOR ( 'NONE', #11324, 1000.000000000000000 ) ;
#18053=DIRECTION ( 'NONE',  ( 0.000000000000000000, 0.000000000000000000, 1.000000000000000000 ) ) ;
#18072=CIRCLE ( 'NONE', #13776, 17.87500000001787726 ) ;
#18073=DIRECTION ( 'NONE',  ( -1.000000000000000000, 0.000000000000000000, 0.000000000000000000 ) ) ;
#18077=VERTEX_POINT ( 'NONE', #9887 ) ;
#18082=FACE_OUTER_BOUND ( 'NONE', #14813, .T. ) ;
#18085=EDGE_LOOP ( 'NONE', ( #7664, #10020, #13368, #22499 ) ) ;
#18107=CARTESIAN_POINT ( 'NONE',  ( 23.00000000000000000, -10.66755332433018744, -4.772587172891147311 ) ) ;
#18125=EDGE_CURVE ( 'NONE', #8876, #13479, #18341, .T. ) ;
#18153=EDGE_CURVE ( 'NONE', #1347, #9461, #8578, .T. ) ;
#18158=AXIS2_PLACEMENT_3D ( 'NONE', #9201, #16650, #24087 ) ;
#18164=CARTESIAN_POINT ( 'NONE',  ( 23.00000000000000000, 17.02535186363804698, 5.445458559199168214 ) ) ;
#18182=AXIS2_PLACEMENT_3D ( 'NONE', #17933, #1221, #10926 ) ;
#18189=EDGE_CURVE ( 'NONE', #4544, #11455, #9750, .T. ) ;
#18194=AXIS2_PLACEMENT_3D ( 'NONE', #2537, #13521, #15695 ) ;
#18209=DIRECTION ( 'NONE',  ( 0.000000000000000000, 0.000000000000000000, 1.000000000000000000 ) ) ;
#18248=EDGE_CURVE ( 'NONE', #19205, #9146, #12851, .T. ) ;
#18270=CARTESIAN_POINT ( 'NONE',  ( 23.00000000000000000, -11.55437235128772500, -1.752358929577761515 ) ) ;
#18271=ADVANCED_FACE ( 'NONE', ( #6944 ), #22306, .T. ) ;
#18276=DIRECTION ( 'NONE',  ( -1.000000000000000000, 0.000000000000000000, 0.000000000000000000 ) ) ;
#18301=VERTEX_POINT ( 'NONE', #16783 ) ;
#18307=DIRECTION ( 'NONE',  ( -1.000000000000000000, 0.000000000000000000, 0.000000000000000000 ) ) ;
#18341=CIRCLE ( 'NONE', #13652, 17.87500000001787726 ) ;
#18365=ORIENTED_EDGE ( 'NONE', *, *, #19323, .T. ) ;
#18380=EDGE_CURVE ( 'NONE', #13723, #23530, #1218, .T. ) ;
#18385=CARTESIAN_POINT ( 'NONE',  ( 0.000000000000000000, 2.967071445750145031, -17.62702788437270840 ) ) ;
#18406=CARTESIAN_POINT ( 'NONE',  ( 0.000000000000000000, -8.772759796005177080, -7.720943453482119523 ) ) ;
#18409=EDGE_CURVE ( 'NONE', #16640, #23003, #10440, .T. ) ;
#18433=AXIS2_PLACEMENT_3D ( 'NONE', #15010, #22365, #5644 ) ;
#18446=CARTESIAN_POINT ( 'NONE',  ( 23.00000000000000000, -13.61176534793449200, 4.089617900950054619 ) ) ;
#18460=DIRECTION ( 'NONE',  ( -1.000000000000000000, 0.000000000000000000, 0.000000000000000000 ) ) ;
#18465=ORIENTED_EDGE ( 'NONE', *, *, #12029, .F. ) ;
#18478=ORIENTED_EDGE ( 'NONE', *, *, #18153, .T. ) ;
#18517=CARTESIAN_POINT ( 'NONE',  ( 23.00000000000000000, -6.393861490227802591, -9.782270569456514409 ) ) ;
#18521=CIRCLE ( 'NONE', #7225, 11.68650000001168721 ) ;
#18533=AXIS2_PLACEMENT_3D ( 'NONE', #658, #11601, #8066 ) ;
#18540=AXIS2_PLACEMENT_3D ( 'NONE', #19304, #1005, #6611 ) ;
#18550=( GEOMETRIC_REPRESENTATION_CONTEXT ( 3 ) GLOBAL_UNCERTAINTY_ASSIGNED_CONTEXT ( ( #6684 ) ) GLOBAL_UNIT_ASSIGNED_CONTEXT ( ( #10220, #12423, #7178 ) ) REPRESENTATION_CONTEXT ( 'NONE', 'WORKASPACE' ) );
#18551=CIRCLE ( 'NONE', #9568, 6.050000000006050982 ) ;
#18557=AXIS2_PLACEMENT_3D ( 'NONE', #10638, #12471, #22138 ) ;
#18570=CIRCLE ( 'NONE', #22472, 6.050000000006050094 ) ;
#18611=CARTESIAN_POINT ( 'NONE',  ( 23.00000000000000000, 10.59264252385243665, -4.936618945406485714 ) ) ;
#18619=EDGE_LOOP ( 'NONE', ( #4643, #10191, #7589, #19000 ) ) ;
#18626=DIRECTION ( 'NONE',  ( 0.000000000000000000, 0.7557495743542551603, 0.6548607339452887643 ) ) ;
#18644=VERTEX_POINT ( 'NONE', #2810 ) ;
#18646=VERTEX_POINT ( 'NONE', #748 ) ;
#18653=FACE_OUTER_BOUND ( 'NONE', #5860, .T. ) ;
#18672=ORIENTED_EDGE ( 'NONE', *, *, #19959, .F. ) ;
#18695=DIRECTION ( 'NONE',  ( 0.000000000000000000, 0.9096319953545193293, -0.4154150130018841591 ) ) ;
#18701=EDGE_CURVE ( 'NONE', #20733, #3712, #15873, .T. ) ;
#18702=VECTOR ( 'NONE', #7313, 1000.000000000000000 ) ;
#18706=CARTESIAN_POINT ( 'NONE',  ( 23.00000000000000000, 11.37860023611340665, 13.78561139983856521 ) ) ;
#18712=DIRECTION ( 'NONE',  ( 0.000000000000000000, 0.7557495743542552713, 0.6548607339452886533 ) ) ;
#18714=FACE_OUTER_BOUND ( 'NONE', #12377, .T. ) ;
#18721=ORIENTED_EDGE ( 'NONE', *, *, #13447, .F. ) ;
#18743=ORIENTED_EDGE ( 'NONE', *, *, #10651, .F. ) ;
#18753=VECTOR ( 'NONE', #10240, 1000.000000000000000 ) ;
#18798=CARTESIAN_POINT ( 'NONE',  ( 23.00000000000000000, -10.66755332433025139, 4.772587172891002538 ) ) ;
#18801=CARTESIAN_POINT ( 'NONE',  ( 23.00000000000000000, 0.000000000000000000, 0.000000000000000000 ) ) ;
#18807=VECTOR ( 'NONE', #13563, 1000.000000000000000 ) ;
#18815=DIRECTION ( 'NONE',  ( -1.000000000000000000, 0.000000000000000000, 0.000000000000000000 ) ) ;
#18872=AXIS2_PLACEMENT_3D ( 'NONE', #1059, #15924, #12253 ) ;
#18878=DIRECTION ( 'NONE',  ( -1.000000000000000000, 0.000000000000000000, 0.000000000000000000 ) ) ;
#18889=DIRECTION ( 'NONE',  ( 0.000000000000000000, 0.000000000000000000, 1.000000000000000000 ) ) ;
#18907=ORIENTED_EDGE ( 'NONE', *, *, #20076, .F. ) ;
#18922=CARTESIAN_POINT ( 'NONE',  ( 0.000000000000000000, 12.02595010061954461, 13.22467954916291433 ) ) ;
#18938=DIRECTION ( 'NONE',  ( 0.000000000000000000, 0.7557495743542552713, 0.6548607339452886533 ) ) ;
#18939=DIRECTION ( 'NONE',  ( 0.000000000000000000, -0.9898214418809342385, 0.1423148382732755957 ) ) ;
#18942=VERTEX_POINT ( 'NONE', #13148 ) ;
#18943=CARTESIAN_POINT ( 'NONE',  ( 23.00000000000000000, 12.00453763395396756, -7.608955687739546114 ) ) ;
#18958=LINE ( 'NONE', #51, #8682 ) ;
#18967=EDGE_CURVE ( 'NONE', #15320, #13734, #2002, .T. ) ;
#18975=DIRECTION ( 'NONE',  ( 0.000000000000000000, 0.000000000000000000, 1.000000000000000000 ) ) ;
#18976=DIRECTION ( 'NONE',  ( -1.000000000000000000, 0.000000000000000000, -0.000000000000000000 ) ) ;
#18988=DIRECTION ( 'NONE',  ( -1.000000000000000000, 0.000000000000000000, 0.000000000000000000 ) ) ;
#18989=ORIENTED_EDGE ( 'NONE', *, *, #6076, .T. ) ;
#19000=ORIENTED_EDGE ( 'NONE', *, *, #2679, .T. ) ;
#19004=CYLINDRICAL_SURFACE ( 'NONE', #8744, 17.87500000001787726 ) ;
#19059=CARTESIAN_POINT ( 'NONE',  ( 23.00000000000000000, 0.000000000000000000, 0.000000000000000000 ) ) ;
#19080=VERTEX_POINT ( 'NONE', #1095 ) ;
#19094=ORIENTED_EDGE ( 'NONE', *, *, #21940, .F. ) ;
#19095=EDGE_CURVE ( 'NONE', #8837, #4471, #21514, .T. ) ;
#19135=CYLINDRICAL_SURFACE ( 'NONE', #6449, 17.87500000001787726 ) ;
#19140=CARTESIAN_POINT ( 'NONE',  ( 23.00000000000000000, -11.55437235128774809, 1.752358929577604085 ) ) ;
#19169=DIRECTION ( 'NONE',  ( -1.000000000000000000, 0.000000000000000000, 0.000000000000000000 ) ) ;
#19181=AXIS2_PLACEMENT_3D ( 'NONE', #7466, #14698, #20560 ) ;
#19199=CARTESIAN_POINT ( 'NONE',  ( 23.00000000000000000, 17.26667456984545623, -4.623588898214384457 ) ) ;
#19200=AXIS2_PLACEMENT_3D ( 'NONE', #15657, #23130, #6413 ) ;
#19202=CYLINDRICAL_SURFACE ( 'NONE', #5595, 17.87500000001787726 ) ;
#19205=VERTEX_POINT ( 'NONE', #18385 ) ;
#19213=CIRCLE ( 'NONE', #8680, 17.87500000001787726 ) ;
#19222=ORIENTED_EDGE ( 'NONE', *, *, #12029, .T. ) ;
#19223=CARTESIAN_POINT ( 'NONE',  ( 0.000000000000000000, 3.378881074890460745, -11.18737882312118082 ) ) ;
#19231=ORIENTED_EDGE ( 'NONE', *, *, #16586, .T. ) ;
#19235=EDGE_CURVE ( 'NONE', #12170, #23563, #3390, .T. ) ;
#19238=AXIS2_PLACEMENT_3D ( 'NONE', #15269, #6025, #4205 ) ;
#19271=DIRECTION ( 'NONE',  ( -1.000000000000000000, 0.000000000000000000, 0.000000000000000000 ) ) ;
#19288=CARTESIAN_POINT ( 'NONE',  ( 0.000000000000000000, 12.00453763395396756, -1.558955687733494244 ) ) ;
#19292=CIRCLE ( 'NONE', #21242, 11.68650000001168721 ) ;
#19304=CARTESIAN_POINT ( 'NONE',  ( 23.00000000000000000, 14.21257171757157245, 0.08908218613057176938 ) ) ;
#19306=AXIS2_PLACEMENT_3D ( 'NONE', #6574, #7031, #3384 ) ;
#19323=EDGE_CURVE ( 'NONE', #20443, #9461, #14357, .T. ) ;
#19345=ORIENTED_EDGE ( 'NONE', *, *, #22146, .F. ) ;
#19359=CIRCLE ( 'NONE', #10372, 11.68650000001168543 ) ;
#19384=DIRECTION ( 'NONE',  ( -1.000000000000000000, 0.000000000000000000, 0.000000000000000000 ) ) ;
#19391=LINE ( 'NONE', #6313, #1277 ) ;
#19411=DIRECTION ( 'NONE',  ( 0.000000000000000000, 0.5406408174555987767, -0.8412535328311804284 ) ) ;
#19423=CARTESIAN_POINT ( 'NONE',  ( 23.00000000000000000, -8.772759796005278332, 7.720943453482002283 ) ) ;
#19424=ORIENTED_EDGE ( 'NONE', *, *, #13219, .T. ) ;
#19441=CARTESIAN_POINT ( 'NONE',  ( 23.00000000000000000, 12.02595010061972403, -13.22467954916275268 ) ) ;
#19460=ORIENTED_EDGE ( 'NONE', *, *, #9608, .T. ) ;
#19462=ADVANCED_FACE ( 'NONE', ( #17270 ), #6429, .T. ) ;
#19502=DIRECTION ( 'NONE',  ( 0.000000000000000000, 0.000000000000000000, -1.000000000000000000 ) ) ;
#19507=DIRECTION ( 'NONE',  ( 0.000000000000000000, -0.7557495743542635980, 0.6548607339452787723 ) ) ;
#19533=CARTESIAN_POINT ( 'NONE',  ( 23.00000000000000000, -13.61176534793449200, 10.13961790095610560 ) ) ;
#19542=ORIENTED_EDGE ( 'NONE', *, *, #6491, .F. ) ;
#19543=DIRECTION ( 'NONE',  ( 0.000000000000000000, 0.9898214418809322401, 0.1423148382732887240 ) ) ;
#19555=ORIENTED_EDGE ( 'NONE', *, *, #13289, .F. ) ;
#19562=ORIENTED_EDGE ( 'NONE', *, *, #23419, .T. ) ;
#19563=DIRECTION ( 'NONE',  ( 1.000000000000000000, -0.000000000000000000, 0.000000000000000000 ) ) ;
#19583=ORIENTED_EDGE ( 'NONE', *, *, #22736, .T. ) ;
#19592=CARTESIAN_POINT ( 'NONE',  ( 23.00000000000000000, -13.61176534793443338, -4.089617900950226925 ) ) ;
#19615=VECTOR ( 'NONE', #5404, 1000.000000000000000 ) ;
#19642=AXIS2_PLACEMENT_3D ( 'NONE', #5600, #16695, #10935 ) ;
#19645=DIRECTION ( 'NONE',  ( -1.000000000000000000, 0.000000000000000000, 0.000000000000000000 ) ) ;
#19660=CIRCLE ( 'NONE', #20416, 17.87500000001787726 ) ;
#19676=CARTESIAN_POINT ( 'NONE',  ( 23.00000000000000000, -0.09016380984455869829, -11.68615217844040721 ) ) ;
#19678=ADVANCED_FACE ( 'NONE', ( #6783 ), #18002, .T. ) ;
#19684=CARTESIAN_POINT ( 'NONE',  ( 0.000000000000000000, 14.21257171757157245, 0.08908218613057176938 ) ) ;
#19687=AXIS2_PLACEMENT_3D ( 'NONE', #23060, #15484, #989 ) ;
#19692=ORIENTED_EDGE ( 'NONE', *, *, #448, .F. ) ;
#19727=ORIENTED_EDGE ( 'NONE', *, *, #22164, .F. ) ;
#19731=AXIS2_PLACEMENT_3D ( 'NONE', #20136, #23681, #1699 ) ;
#19734=CIRCLE ( 'NONE', #14238, 11.68650000001168721 ) ;
#19759=EDGE_CURVE ( 'NONE', #22524, #13479, #752, .T. ) ;
#19763=AXIS2_PLACEMENT_3D ( 'NONE', #19684, #12210, #6734 ) ;
#19776=CYLINDRICAL_SURFACE ( 'NONE', #18182, 9.000000000000000000 ) ;
#19778=EDGE_CURVE ( 'NONE', #16640, #15261, #14396, .T. ) ;
#19790=ORIENTED_EDGE ( 'NONE', *, *, #21804, .T. ) ;
#19797=DIRECTION ( 'NONE',  ( 0.000000000000000000, 0.000000000000000000, -1.000000000000000000 ) ) ;
#19833=CARTESIAN_POINT ( 'NONE',  ( 23.00000000000000000, 0.000000000000000000, 0.000000000000000000 ) ) ;
#19836=DIRECTION ( 'NONE',  ( 0.000000000000000000, -0.9096319953545137782, -0.4154150130018967602 ) ) ;
#19867=AXIS2_PLACEMENT_3D ( 'NONE', #16041, #20082, #1645 ) ;
#19887=DIRECTION ( 'NONE',  ( 0.000000000000000000, -0.9096319953545137782, -0.4154150130018965936 ) ) ;
#19901=CARTESIAN_POINT ( 'NONE',  ( 23.00000000000000000, 2.967071445750139702, -17.62702788437271550 ) ) ;
#19914=CARTESIAN_POINT ( 'NONE',  ( 0.000000000000000000, 5.985147671565880678, -12.89120389306408754 ) ) ;
#19917=ORIENTED_EDGE ( 'NONE', *, *, #183, .F. ) ;
#19920=ORIENTED_EDGE ( 'NONE', *, *, #10651, .T. ) ;
#19921=EDGE_LOOP ( 'NONE', ( #1167, #17489, #16324, #6134 ) ) ;
#19922=DIRECTION ( 'NONE',  ( -1.000000000000000000, 0.000000000000000000, 0.000000000000000000 ) ) ;
#19925=VERTEX_POINT ( 'NONE', #19901 ) ;
#19932=EDGE_CURVE ( 'NONE', #4776, #23202, #10601, .T. ) ;
#19934=EDGE_CURVE ( 'NONE', #11737, #18644, #22220, .T. ) ;
#19951=CYLINDRICAL_SURFACE ( 'NONE', #14521, 6.050000000006050982 ) ;
#19959=EDGE_CURVE ( 'NONE', #18301, #14710, #2699, .T. ) ;
#19972=ORIENTED_EDGE ( 'NONE', *, *, #448, .T. ) ;
#19991=DIRECTION ( 'NONE',  ( 0.000000000000000000, 0.000000000000000000, 1.000000000000000000 ) ) ;
#20014=EDGE_CURVE ( 'NONE', #12041, #22524, #11266, .T. ) ;
#20016=ORIENTED_EDGE ( 'NONE', *, *, #19323, .F. ) ;
#20022=LINE ( 'NONE', #12801, #18702 ) ;
#20046=CIRCLE ( 'NONE', #15745, 11.68650000001168721 ) ;
#20050=ADVANCED_FACE ( 'NONE', ( #4663 ), #3656, .T. ) ;
#20052=VECTOR ( 'NONE', #19922, 1000.000000000000000 ) ;
#20054=CARTESIAN_POINT ( 'NONE',  ( 0.000000000000000000, 0.000000000000000000, 0.000000000000000000 ) ) ;
#20056=CARTESIAN_POINT ( 'NONE',  ( 0.000000000000000000, 17.02535186363803632, 5.445458559199173543 ) ) ;
#20071=AXIS2_PLACEMENT_3D ( 'NONE', #10932, #1824, #16570 ) ;
#20076=EDGE_CURVE ( 'NONE', #21535, #15398, #20022, .T. ) ;
#20082=DIRECTION ( 'NONE',  ( -1.000000000000000000, -0.000000000000000000, -0.000000000000000000 ) ) ;
#20100=ORIENTED_EDGE ( 'NONE', *, *, #21263, .F. ) ;
#20113=CIRCLE ( 'NONE', #18557, 6.050000000006050094 ) ;
#20117=FACE_OUTER_BOUND ( 'NONE', #11377, .T. ) ;
#20136=CARTESIAN_POINT ( 'NONE',  ( 23.00000000000000000, 0.000000000000000000, 0.000000000000000000 ) ) ;
#20163=CARTESIAN_POINT ( 'NONE',  ( 23.00000000000000000, -8.772759796005278332, 7.720943453482002283 ) ) ;
#20166=VERTEX_POINT ( 'NONE', #8900 ) ;
#20172=DIRECTION ( 'NONE',  ( -1.000000000000000000, -0.000000000000000000, -0.000000000000000000 ) ) ;
#20187=ORIENTED_EDGE ( 'NONE', *, *, #20204, .F. ) ;
#20191=ORIENTED_EDGE ( 'NONE', *, *, #6468, .F. ) ;
#20195=DIRECTION ( 'NONE',  ( -1.000000000000000000, 0.000000000000000000, 0.000000000000000000 ) ) ;
#20204=EDGE_CURVE ( 'NONE', #20932, #20166, #16236, .T. ) ;
#20229=CARTESIAN_POINT ( 'NONE',  ( 23.00000000000000000, -15.26463740537730907, 9.300885435430052084 ) ) ;
#20258=CARTESIAN_POINT ( 'NONE',  ( 0.000000000000000000, -15.26463740537718827, -9.300885435430258141 ) ) ;
#20260=CIRCLE ( 'NONE', #23347, 11.68650000001168721 ) ;
#20265=AXIS2_PLACEMENT_3D ( 'NONE', #18801, #15233, #5995 ) ;
#20283=VERTEX_POINT ( 'NONE', #9481 ) ;
#20284=LINE ( 'NONE', #7099, #10613 ) ;
#20286=ORIENTED_EDGE ( 'NONE', *, *, #8172, .T. ) ;
#20289=DIRECTION ( 'NONE',  ( -1.000000000000000000, -0.000000000000000000, -0.000000000000000000 ) ) ;
#20329=CARTESIAN_POINT ( 'NONE',  ( 11.50000000000000000, 17.26667456984545268, -4.623588898214372023 ) ) ;
#20335=EDGE_CURVE ( 'NONE', #14903, #21740, #4268, .T. ) ;
#20339=LINE ( 'NONE', #18517, #17581 ) ;
#20368=DIRECTION ( 'NONE',  ( 0.000000000000000000, 0.000000000000000000, 1.000000000000000000 ) ) ;
#20378=AXIS2_PLACEMENT_3D ( 'NONE', #22384, #16742, #24075 ) ;
#20391=VECTOR ( 'NONE', #17671, 1000.000000000000000 ) ;
#20404=FACE_OUTER_BOUND ( 'NONE', #15212, .T. ) ;
#20405=CARTESIAN_POINT ( 'NONE',  ( 0.000000000000000000, 2.119223430970168742, 17.74893002550480858 ) ) ;
#20416=AXIS2_PLACEMENT_3D ( 'NONE', #17912, #3136, #8613 ) ;
#20431=LINE ( 'NONE', #13216, #6773 ) ;
#20443=VERTEX_POINT ( 'NONE', #21463 ) ;
#20453=CARTESIAN_POINT ( 'NONE',  ( 23.00000000000000000, -13.61176534793449200, 4.089617900950054619 ) ) ;
#20465=CARTESIAN_POINT ( 'NONE',  ( 23.00000000000000000, 14.21257171757157245, 0.08908218613057176938 ) ) ;
#20512=CARTESIAN_POINT ( 'NONE',  ( 23.00000000000000000, 0.000000000000000000, 0.000000000000000000 ) ) ;
#20528=CARTESIAN_POINT ( 'NONE',  ( 0.000000000000000000, 0.000000000000000000, 0.000000000000000000 ) ) ;
#20533=AXIS2_PLACEMENT_3D ( 'NONE', #15616, #21265, #4561 ) ;
#20535=CARTESIAN_POINT ( 'NONE',  ( 23.00000000000000000, -10.66755332433018744, -4.772587172891147311 ) ) ;
#20542=CYLINDRICAL_SURFACE ( 'NONE', #15033, 6.050000000006050982 ) ;
#20553=CARTESIAN_POINT ( 'NONE',  ( 0.000000000000000000, -0.09016380984471504545, 11.68615217844040721 ) ) ;
#20560=DIRECTION ( 'NONE',  ( 0.000000000000000000, 0.9096319953545194403, -0.4154150130018842146 ) ) ;
#20581=CARTESIAN_POINT ( 'NONE',  ( 23.00000000000000000, -13.66196005206966468, 3.918670437617043145 ) ) ;
#20590=DIRECTION ( 'NONE',  ( 0.000000000000000000, 0.000000000000000000, 1.000000000000000000 ) ) ;
#20591=ADVANCED_FACE ( 'NONE', ( #5464 ), #1566, .T. ) ;
#20596=ORIENTED_EDGE ( 'NONE', *, *, #6372, .T. ) ;
#20629=DIRECTION ( 'NONE',  ( 0.000000000000000000, 0.000000000000000000, 1.000000000000000000 ) ) ;
#20640=LINE ( 'NONE', #12941, #18038 ) ;
#20645=DIRECTION ( 'NONE',  ( 1.000000000000000000, 0.000000000000000000, -0.000000000000000000 ) ) ;
#20652=VERTEX_POINT ( 'NONE', #1337 ) ;
#20658=ORIENTED_EDGE ( 'NONE', *, *, #17512, .F. ) ;
#20663=ADVANCED_FACE ( 'NONE', ( #8391 ), #4995, .T. ) ;
#20664=VERTEX_POINT ( 'NONE', #23416 ) ;
#20690=CYLINDRICAL_SURFACE ( 'NONE', #11597, 6.050000000006052758 ) ;
#20692=DIRECTION ( 'NONE',  ( -1.000000000000000000, -0.000000000000000000, -0.000000000000000000 ) ) ;
#20697=DIRECTION ( 'NONE',  ( -1.000000000000000000, 0.000000000000000000, 0.000000000000000000 ) ) ;
#20717=EDGE_CURVE ( 'NONE', #12170, #12203, #2134, .T. ) ;
#20722=CARTESIAN_POINT ( 'NONE',  ( -10.00000000000000000, 0.000000000000000000, 0.000000000000000000 ) ) ;
#20730=CARTESIAN_POINT ( 'NONE',  ( 23.00000000000000000, 0.000000000000000000, 0.000000000000000000 ) ) ;
#20733=VERTEX_POINT ( 'NONE', #11922 ) ;
#20747=DIRECTION ( 'NONE',  ( 1.000000000000000000, 0.000000000000000000, -0.000000000000000000 ) ) ;
#20770=DIRECTION ( 'NONE',  ( 0.000000000000000000, -0.9898214418809341275, 0.1423148382732755679 ) ) ;
#20779=CIRCLE ( 'NONE', #12199, 6.050000000006050982 ) ;
#20780=EDGE_CURVE ( 'NONE', #9461, #1347, #11445, .T. ) ;
#20806=CIRCLE ( 'NONE', #23152, 6.050000000006051870 ) ;
#20829=VERTEX_POINT ( 'NONE', #11524 ) ;
#20837=FACE_OUTER_BOUND ( 'NONE', #11442, .T. ) ;
#20851=EDGE_CURVE ( 'NONE', #5942, #12689, #2522, .T. ) ;
#20884=CIRCLE ( 'NONE', #4130, 6.050000000006052758 ) ;
#20888=CARTESIAN_POINT ( 'NONE',  ( 23.00000000000000000, 0.000000000000000000, 0.000000000000000000 ) ) ;
#20921=DIRECTION ( 'NONE',  ( 0.000000000000000000, 0.000000000000000000, 1.000000000000000000 ) ) ;
#20929=CYLINDRICAL_SURFACE ( 'NONE', #14643, 11.68650000001168721 ) ;
#20932=VERTEX_POINT ( 'NONE', #15170 ) ;
#20949=ADVANCED_FACE ( 'NONE', ( #3744 ), #11152, .T. ) ;
#20952=DIRECTION ( 'NONE',  ( 0.000000000000000000, 0.000000000000000000, 1.000000000000000000 ) ) ;
#20973=VERTEX_POINT ( 'NONE', #12003 ) ;
#20980=CIRCLE ( 'NONE', #10452, 6.050000000006051870 ) ;
#20990=ORIENTED_EDGE ( 'NONE', *, *, #11168, .T. ) ;
#21017=ORIENTED_EDGE ( 'NONE', *, *, #591, .F. ) ;
#21022=ORIENTED_EDGE ( 'NONE', *, *, #2573, .F. ) ;
#21023=AXIS2_PLACEMENT_3D ( 'NONE', #13617, #7993, #13870 ) ;
#21030=DIRECTION ( 'NONE',  ( -1.000000000000000000, 0.000000000000000000, 0.000000000000000000 ) ) ;
#21077=DIRECTION ( 'NONE',  ( -1.000000000000000000, -0.000000000000000000, -0.000000000000000000 ) ) ;
#21082=CYLINDRICAL_SURFACE ( 'NONE', #5592, 6.050000000006051870 ) ;
#21105=CIRCLE ( 'NONE', #21503, 9.000000000000000000 ) ;
#21111=DIRECTION ( 'NONE',  ( -1.000000000000000000, -0.000000000000000000, 0.000000000000000000 ) ) ;
#21115=DIRECTION ( 'NONE',  ( -1.000000000000000000, 0.000000000000000000, 0.000000000000000000 ) ) ;
#21131=EDGE_CURVE ( 'NONE', #8700, #6008, #11295, .T. ) ;
#21140=AXIS2_PLACEMENT_3D ( 'NONE', #12112, #11421, #16930 ) ;
#21170=ADVANCED_FACE ( 'NONE', ( #13147 ), #19135, .T. ) ;
#21173=DIRECTION ( 'NONE',  ( 0.000000000000000000, 0.000000000000000000, -1.000000000000000000 ) ) ;
#21212=CARTESIAN_POINT ( 'NONE',  ( 0.000000000000000000, 2.119223430970397004, -17.74893002550478016 ) ) ;
#21220=ORIENTED_EDGE ( 'NONE', *, *, #19235, .T. ) ;
#21223=ORIENTED_EDGE ( 'NONE', *, *, #9676, .T. ) ;
#21242=AXIS2_PLACEMENT_3D ( 'NONE', #4453, #23249, #1041 ) ;
#21263=EDGE_CURVE ( 'NONE', #4471, #15821, #10261, .T. ) ;
#21265=DIRECTION ( 'NONE',  ( -1.000000000000000000, -0.000000000000000000, -0.000000000000000000 ) ) ;
#21273=CIRCLE ( 'NONE', #3346, 6.050000000006051870 ) ;
#21281=AXIS2_PLACEMENT_3D ( 'NONE', #16062, #18023, #14459 ) ;
#21287=ORIENTED_EDGE ( 'NONE', *, *, #16336, .F. ) ;
#21305=CARTESIAN_POINT ( 'NONE',  ( 23.00000000000000000, -8.772759796005177080, -7.720943453482119523 ) ) ;
#21375=ORIENTED_EDGE ( 'NONE', *, *, #23948, .F. ) ;
#21380=DIRECTION ( 'NONE',  ( -1.000000000000000000, 0.000000000000000000, 0.000000000000000000 ) ) ;
#21385=CIRCLE ( 'NONE', #7714, 11.68650000001168721 ) ;
#21399=VERTEX_POINT ( 'NONE', #22228 ) ;
#21410=CARTESIAN_POINT ( 'NONE',  ( 0.000000000000000000, -14.80154252341802490, 10.02147513732818851 ) ) ;
#21459=CARTESIAN_POINT ( 'NONE',  ( 23.00000000000000000, 11.90821470209324140, 7.758837095328885880 ) ) ;
#21463=CARTESIAN_POINT ( 'NONE',  ( 23.00000000000000000, 0.000000000000000000, 9.000000000000000000 ) ) ;
#21464=ORIENTED_EDGE ( 'NONE', *, *, #17278, .T. ) ;
#21467=ORIENTED_EDGE ( 'NONE', *, *, #21263, .T. ) ;
#21471=ADVANCED_FACE ( 'NONE', ( #6864 ), #16475, .T. ) ;
#21501=AXIS2_PLACEMENT_3D ( 'NONE', #20528, #20172, #14879 ) ;
#21503=AXIS2_PLACEMENT_3D ( 'NONE', #23394, #16042, #12127 ) ;
#21514=CIRCLE ( 'NONE', #6710, 11.68650000001168898 ) ;
#21521=CIRCLE ( 'NONE', #21914, 11.68650000001168721 ) ;
#21535=VERTEX_POINT ( 'NONE', #13053 ) ;
#21537=CIRCLE ( 'NONE', #10202, 6.050000000006050982 ) ;
#21580=DIRECTION ( 'NONE',  ( 0.000000000000000000, 0.000000000000000000, 1.000000000000000000 ) ) ;
#21582=CIRCLE ( 'NONE', #152, 6.050000000006050982 ) ;
#21605=DIRECTION ( 'NONE',  ( 1.000000000000000000, 0.000000000000000000, -0.000000000000000000 ) ) ;
#21640=ORIENTED_EDGE ( 'NONE', *, *, #19235, .F. ) ;
#21662=EDGE_LOOP ( 'NONE', ( #22518, #197, #2715, #23115 ) ) ;
#21668=FACE_OUTER_BOUND ( 'NONE', #23161, .T. ) ;
#21689=CARTESIAN_POINT ( 'NONE',  ( 11.50000000000000000, 17.26667456984545979, 4.623588898214379128 ) ) ;
#21707=DIRECTION ( 'NONE',  ( -1.000000000000000000, 0.000000000000000000, 0.000000000000000000 ) ) ;
#21714=ORIENTED_EDGE ( 'NONE', *, *, #591, .T. ) ;
#21715=CARTESIAN_POINT ( 'NONE',  ( 0.000000000000000000, -17.86986844953241516, -0.4282833139928939881 ) ) ;
#21718=ORIENTED_EDGE ( 'NONE', *, *, #11168, .F. ) ;
#21740=VERTEX_POINT ( 'NONE', #2569 ) ;
#21742=ORIENTED_EDGE ( 'NONE', *, *, #17819, .T. ) ;
#21781=DIRECTION ( 'NONE',  ( 0.000000000000000000, 0.5406408174555985546, -0.8412535328311806504 ) ) ;
#21804=EDGE_CURVE ( 'NONE', #1531, #22050, #18551, .T. ) ;
#21818=LINE ( 'NONE', #17924, #15242 ) ;
#21837=ADVANCED_FACE ( 'NONE', ( #8891 ), #12428, .T. ) ;
#21846=CARTESIAN_POINT ( 'NONE',  ( 23.00000000000000000, 3.378881074890309311, 11.18737882312122878 ) ) ;
#21914=AXIS2_PLACEMENT_3D ( 'NONE', #23367, #17480, #8568 ) ;
#21931=EDGE_CURVE ( 'NONE', #18942, #20443, #11112, .T. ) ;
#21934=DIRECTION ( 'NONE',  ( -1.000000000000000000, 0.000000000000000000, 0.000000000000000000 ) ) ;
#21938=AXIS2_PLACEMENT_3D ( 'NONE', #8050, #21115, #2589 ) ;
#21940=EDGE_CURVE ( 'NONE', #11642, #1246, #10828, .T. ) ;
#21944=DIRECTION ( 'NONE',  ( 0.000000000000000000, 0.000000000000000000, 1.000000000000000000 ) ) ;
#21953=CIRCLE ( 'NONE', #11393, 6.050000000006050982 ) ;
#21985=CARTESIAN_POINT ( 'NONE',  ( 0.000000000000000000, 0.000000000000000000, 0.000000000000000000 ) ) ;
#22006=VERTEX_POINT ( 'NONE', #12899 ) ;
#22022=EDGE_LOOP ( 'NONE', ( #22762, #18672, #15783, #22232 ) ) ;
#22027=VERTEX_POINT ( 'NONE', #14846 ) ;
#22034=EDGE_CURVE ( 'NONE', #15534, #12989, #20884, .T. ) ;
#22046=CIRCLE ( 'NONE', #1006, 11.68650000001168898 ) ;
#22050=VERTEX_POINT ( 'NONE', #13255 ) ;
#22075=CIRCLE ( 'NONE', #10367, 6.050000000006050982 ) ;
#22083=FACE_OUTER_BOUND ( 'NONE', #11395, .T. ) ;
#22092=ADVANCED_FACE ( 'NONE', ( #18653 ), #1928, .T. ) ;
#22101=AXIS2_PLACEMENT_3D ( 'NONE', #19833, #14316, #21781 ) ;
#22138=DIRECTION ( 'NONE',  ( 0.000000000000000000, -0.5406408174555870083, -0.8412535328311879779 ) ) ;
#22145=ORIENTED_EDGE ( 'NONE', *, *, #13219, .F. ) ;
#22146=EDGE_CURVE ( 'NONE', #12203, #12368, #14274, .T. ) ;
#22155=DIRECTION ( 'NONE',  ( 0.000000000000000000, 0.2817325568414236758, 0.9594929736144991450 ) ) ;
#22164=EDGE_CURVE ( 'NONE', #1531, #15821, #2203, .T. ) ;
#22198=ORIENTED_EDGE ( 'NONE', *, *, #23780, .F. ) ;
#22200=CARTESIAN_POINT ( 'NONE',  ( 23.00000000000000000, -11.55437235128774809, 1.752358929577604085 ) ) ;
#22204=CYLINDRICAL_SURFACE ( 'NONE', #19642, 6.050000000006051870 ) ;
#22208=ORIENTED_EDGE ( 'NONE', *, *, #18125, .F. ) ;
#22215=VECTOR ( 'NONE', #3131, 1000.000000000000000 ) ;
#22220=CIRCLE ( 'NONE', #12462, 6.050000000006052758 ) ;
#22228=CARTESIAN_POINT ( 'NONE',  ( 23.00000000000000000, 2.967071445749909220, 17.62702788437275458 ) ) ;
#22229=EDGE_CURVE ( 'NONE', #23202, #19080, #19359, .T. ) ;
#22232=ORIENTED_EDGE ( 'NONE', *, *, #13314, .T. ) ;
#22234=AXIS2_PLACEMENT_3D ( 'NONE', #18943, #18460, #9284 ) ;
#22238=CARTESIAN_POINT ( 'NONE',  ( 23.00000000000000000, -13.66196005206961850, -3.918670437617226110 ) ) ;
#22253=DIRECTION ( 'NONE',  ( -1.000000000000000000, 0.000000000000000000, 0.000000000000000000 ) ) ;
#22294=DIRECTION ( 'NONE',  ( -1.000000000000000000, -0.000000000000000000, 0.000000000000000000 ) ) ;
#22304=CIRCLE ( 'NONE', #8258, 11.68650000001168898 ) ;
#22306=CYLINDRICAL_SURFACE ( 'NONE', #9755, 11.68650000001168721 ) ;
#22319=AXIS2_PLACEMENT_3D ( 'NONE', #7207, #14650, #12811 ) ;
#22344=DIRECTION ( 'NONE',  ( 0.000000000000000000, 0.000000000000000000, 1.000000000000000000 ) ) ;
#22354=FACE_OUTER_BOUND ( 'NONE', #12256, .T. ) ;
#22365=DIRECTION ( 'NONE',  ( -1.000000000000000000, -0.000000000000000000, -0.000000000000000000 ) ) ;
#22376=VECTOR ( 'NONE', #284, 1000.000000000000000 ) ;
#22384=CARTESIAN_POINT ( 'NONE',  ( 23.00000000000000000, -9.374578970469563899, -10.68280860024325030 ) ) ;
#22414=DIRECTION ( 'NONE',  ( 0.000000000000000000, -0.9898214418809342385, 0.1423148382732755957 ) ) ;
#22415=DIRECTION ( 'NONE',  ( -1.000000000000000000, 0.000000000000000000, 0.000000000000000000 ) ) ;
#22418=EDGE_CURVE ( 'NONE', #20829, #13157, #8440, .T. ) ;
#22427=CYLINDRICAL_SURFACE ( 'NONE', #17656, 6.050000000006051870 ) ;
#22472=AXIS2_PLACEMENT_3D ( 'NONE', #7382, #7737, #18626 ) ;
#22494=CARTESIAN_POINT ( 'NONE',  ( 23.00000000000000000, -7.812991839788868909, 16.07708877602010489 ) ) ;
#22499=ORIENTED_EDGE ( 'NONE', *, *, #22586, .T. ) ;
#22507=ORIENTED_EDGE ( 'NONE', *, *, #17278, .F. ) ;
#22518=ORIENTED_EDGE ( 'NONE', *, *, #19759, .T. ) ;
#22524=VERTEX_POINT ( 'NONE', #9186 ) ;
#22529=EDGE_CURVE ( 'NONE', #10776, #11642, #24031, .T. ) ;
#22536=DIRECTION ( 'NONE',  ( -1.000000000000000000, -0.000000000000000000, 0.000000000000000000 ) ) ;
#22548=ORIENTED_EDGE ( 'NONE', *, *, #3668, .T. ) ;
#22581=ORIENTED_EDGE ( 'NONE', *, *, #21804, .F. ) ;
#22586=EDGE_CURVE ( 'NONE', #20973, #2336, #15788, .T. ) ;
#22588=CARTESIAN_POINT ( 'NONE',  ( 11.50000000000000000, 11.37860023611358962, -13.78561139983841599 ) ) ;
#22622=DIRECTION ( 'NONE',  ( -1.000000000000000000, -0.000000000000000000, 0.000000000000000000 ) ) ;
#22638=DIRECTION ( 'NONE',  ( -1.000000000000000000, -0.000000000000000000, -0.000000000000000000 ) ) ;
#22689=VECTOR ( 'NONE', #20747, 1000.000000000000000 ) ;
#22700=EDGE_LOOP ( 'NONE', ( #13879, #7545, #22945, #4123 ) ) ;
#22733=ORIENTED_EDGE ( 'NONE', *, *, #8492, .T. ) ;
#22734=ORIENTED_EDGE ( 'NONE', *, *, #22229, .T. ) ;
#22736=EDGE_CURVE ( 'NONE', #10776, #12175, #4910, .T. ) ;
#22762=ORIENTED_EDGE ( 'NONE', *, *, #6631, .F. ) ;
#22767=ORIENTED_EDGE ( 'NONE', *, *, #9368, .F. ) ;
#22784=CARTESIAN_POINT ( 'NONE',  ( 0.000000000000000000, -9.374578970469700678, 10.68280860024311885 ) ) ;
#22798=AXIS2_PLACEMENT_3D ( 'NONE', #11535, #7505, #20590 ) ;
#22809=ORIENTED_EDGE ( 'NONE', *, *, #6236, .T. ) ;
#22819=ORIENTED_EDGE ( 'NONE', *, *, #20851, .F. ) ;
#22832=EDGE_CURVE ( 'NONE', #20166, #23563, #8399, .T. ) ;
#22844=DIRECTION ( 'NONE',  ( -1.000000000000000000, 0.000000000000000000, 0.000000000000000000 ) ) ;
#22845=VECTOR ( 'NONE', #8955, 1000.000000000000000 ) ;
#22860=EDGE_CURVE ( 'NONE', #12368, #20829, #17826, .T. ) ;
#22895=DIRECTION ( 'NONE',  ( 0.000000000000000000, 0.7557495743542551603, 0.6548607339452887643 ) ) ;
#22928=DIRECTION ( 'NONE',  ( -1.000000000000000000, -0.000000000000000000, -0.000000000000000000 ) ) ;
#22945=ORIENTED_EDGE ( 'NONE', *, *, #17660, .T. ) ;
#22958=LINE ( 'NONE', #865, #7117 ) ;
#22968=CARTESIAN_POINT ( 'NONE',  ( 0.000000000000000000, 0.000000000000000000, 0.000000000000000000 ) ) ;
#22983=ORIENTED_EDGE ( 'NONE', *, *, #24077, .F. ) ;
#22992=DIRECTION ( 'NONE',  ( 0.000000000000000000, 0.000000000000000000, -1.000000000000000000 ) ) ;
#22994=DIRECTION ( 'NONE',  ( 0.000000000000000000, 0.000000000000000000, 1.000000000000000000 ) ) ;
#23002=ORIENTED_EDGE ( 'NONE', *, *, #14597, .F. ) ;
#23003=VERTEX_POINT ( 'NONE', #3443 ) ;
#23012=DIRECTION ( 'NONE',  ( -1.000000000000000000, -0.000000000000000000, -0.000000000000000000 ) ) ;
#23033=DIRECTION ( 'NONE',  ( 0.000000000000000000, 0.000000000000000000, 1.000000000000000000 ) ) ;
#23050=CIRCLE ( 'NONE', #16395, 6.050000000006053646 ) ;
#23053=DIRECTION ( 'NONE',  ( 0.000000000000000000, -0.2817325568414366654, 0.9594929736144953702 ) ) ;
#23060=CARTESIAN_POINT ( 'NONE',  ( 0.000000000000000000, 5.985147671565707483, 12.89120389306417103 ) ) ;
#23081=DIRECTION ( 'NONE',  ( -1.000000000000000000, -0.000000000000000000, -0.000000000000000000 ) ) ;
#23104=ORIENTED_EDGE ( 'NONE', *, *, #135, .T. ) ;
#23106=CIRCLE ( 'NONE', #19200, 6.050000000006050982 ) ;
#23111=EDGE_LOOP ( 'NONE', ( #10107, #22548, #17325, #19555 ) ) ;
#23115=ORIENTED_EDGE ( 'NONE', *, *, #20014, .T. ) ;
#23116=ORIENTED_EDGE ( 'NONE', *, *, #135, .F. ) ;
#23130=DIRECTION ( 'NONE',  ( 1.000000000000000000, 0.000000000000000000, 0.000000000000000000 ) ) ;
#23134=CARTESIAN_POINT ( 'NONE',  ( 0.000000000000000000, 0.000000000000000000, 0.000000000000000000 ) ) ;
#23152=AXIS2_PLACEMENT_3D ( 'NONE', #3590, #11010, #7260 ) ;
#23158=EDGE_LOOP ( 'NONE', ( #23002, #6304, #11114, #14732 ) ) ;
#23161=EDGE_LOOP ( 'NONE', ( #13003, #1896, #6003, #10605 ) ) ;
#23188=FACE_OUTER_BOUND ( 'NONE', #6600, .T. ) ;
#23189=AXIS2_PLACEMENT_3D ( 'NONE', #21459, #1093, #4750 ) ;
#23197=DIRECTION ( 'NONE',  ( 0.000000000000000000, 0.000000000000000000, 1.000000000000000000 ) ) ;
#23202=VERTEX_POINT ( 'NONE', #958 ) ;
#23234=CIRCLE ( 'NONE', #16966, 6.050000000006050982 ) ;
#23249=DIRECTION ( 'NONE',  ( -1.000000000000000000, 0.000000000000000000, 0.000000000000000000 ) ) ;
#23293=EDGE_LOOP ( 'NONE', ( #6377, #22507, #12044, #404, #15738, #6988, #6751, #17364, #4866, #24053, #7969, #17610, #7217, #21718, #8935, #735, #22983, #10321, #22198, #15318, #2142, #7400, #9171, #7944, #18721, #22208, #435, #11565, #13566, #7721, #3428, #8527, #6699, #20191, #3052, #6650, #6972, #17129, #12627, #19345, #7280, #22145, #12226, #22767, #2720, #8082, #14959, #21375 ) ) ;
#23347=AXIS2_PLACEMENT_3D ( 'NONE', #13778, #13540, #23053 ) ;
#23363=EDGE_CURVE ( 'NONE', #12175, #13723, #5310, .T. ) ;
#23367=CARTESIAN_POINT ( 'NONE',  ( 0.000000000000000000, 0.000000000000000000, 0.000000000000000000 ) ) ;
#23377=AXIS2_PLACEMENT_3D ( 'NONE', #19059, #2333, #7562 ) ;
#23394=CARTESIAN_POINT ( 'NONE',  ( 23.00000000000000000, 0.000000000000000000, 0.000000000000000000 ) ) ;
#23396=CARTESIAN_POINT ( 'NONE',  ( 23.00000000000000000, 17.02535186363812514, -5.445458559198938175 ) ) ;
#23413=FACE_OUTER_BOUND ( 'NONE', #11667, .T. ) ;
#23416=CARTESIAN_POINT ( 'NONE',  ( 23.00000000000000000, -15.26463740537718827, -9.300885435430258141 ) ) ;
#23419=EDGE_CURVE ( 'NONE', #23514, #5942, #14939, .T. ) ;
#23436=DIRECTION ( 'NONE',  ( -1.000000000000000000, 0.000000000000000000, 0.000000000000000000 ) ) ;
#23449=DIRECTION ( 'NONE',  ( -1.000000000000000000, -0.000000000000000000, 0.000000000000000000 ) ) ;
#23461=EDGE_CURVE ( 'NONE', #11156, #15083, #1794, .T. ) ;
#23498=AXIS2_PLACEMENT_3D ( 'NONE', #5875, #2098, #18695 ) ;
#23514=VERTEX_POINT ( 'NONE', #9220 ) ;
#23519=LINE ( 'NONE', #21689, #22215 ) ;
#23530=VERTEX_POINT ( 'NONE', #9571 ) ;
#23556=EDGE_CURVE ( 'NONE', #20733, #4776, #18570, .T. ) ;
#23563=VERTEX_POINT ( 'NONE', #85 ) ;
#23567=DIRECTION ( 'NONE',  ( 0.000000000000000000, 0.000000000000000000, -1.000000000000000000 ) ) ;
#23575=CIRCLE ( 'NONE', #964, 6.050000000006051870 ) ;
#23590=CIRCLE ( 'NONE', #16168, 6.050000000006052758 ) ;
#23630=CARTESIAN_POINT ( 'NONE',  ( 23.00000000000000000, -13.66196005206961850, -3.918670437617226110 ) ) ;
#23631=CARTESIAN_POINT ( 'NONE',  ( 0.000000000000000000, 0.000000000000000000, 0.000000000000000000 ) ) ;
#23643=EDGE_CURVE ( 'NONE', #1246, #23953, #22075, .T. ) ;
#23673=DIRECTION ( 'NONE',  ( 0.000000000000000000, 0.000000000000000000, -1.000000000000000000 ) ) ;
#23679=DIRECTION ( 'NONE',  ( -1.000000000000000000, 0.000000000000000000, -0.000000000000000000 ) ) ;
#23681=DIRECTION ( 'NONE',  ( 1.000000000000000000, 0.000000000000000000, 0.000000000000000000 ) ) ;
#23704=DIRECTION ( 'NONE',  ( 0.000000000000000000, -0.5406408174555871193, -0.8412535328311879779 ) ) ;
#23733=CARTESIAN_POINT ( 'NONE',  ( 0.000000000000000000, -1.934484387511856252, -14.08058594723508072 ) ) ;
#23734=DIRECTION ( 'NONE',  ( -1.000000000000000000, -0.000000000000000000, 0.000000000000000000 ) ) ;
#23780=EDGE_CURVE ( 'NONE', #12468, #8700, #1829, .T. ) ;
#23785=FACE_OUTER_BOUND ( 'NONE', #13775, .T. ) ;
#23790=EDGE_LOOP ( 'NONE', ( #4153, #1108, #14384, #11246 ) ) ;
#23814=ADVANCED_FACE ( 'NONE', ( #13075 ), #20542, .T. ) ;
#23832=ORIENTED_EDGE ( 'NONE', *, *, #6348, .F. ) ;
#23839=DIRECTION ( 'NONE',  ( 0.000000000000000000, -0.9898214418809341275, 0.1423148382732755679 ) ) ;
#23843=LINE ( 'NONE', #14433, #11116 ) ;
#23863=VECTOR ( 'NONE', #20645, 1000.000000000000000 ) ;
#23870=CARTESIAN_POINT ( 'NONE',  ( 23.00000000000000000, 0.000000000000000000, 0.000000000000000000 ) ) ;
#23900=EDGE_CURVE ( 'NONE', #12989, #5706, #10386, .T. ) ;
#23927=VERTEX_POINT ( 'NONE', #2958 ) ;
#23936=CARTESIAN_POINT ( 'NONE',  ( 23.00000000000000000, -13.61176534793443338, -4.089617900950226925 ) ) ;
#23942=AXIS2_PLACEMENT_3D ( 'NONE', #7904, #17184, #4276 ) ;
#23948=EDGE_CURVE ( 'NONE', #7640, #1246, #6897, .T. ) ;
#23953=VERTEX_POINT ( 'NONE', #13682 ) ;
#23967=DIRECTION ( 'NONE',  ( 0.000000000000000000, 0.000000000000000000, -1.000000000000000000 ) ) ;
#24031=CIRCLE ( 'NONE', #7987, 6.050000000006050982 ) ;
#24053=ORIENTED_EDGE ( 'NONE', *, *, #18967, .F. ) ;
#24059=ORIENTED_EDGE ( 'NONE', *, *, #20204, .T. ) ;
#24060=LINE ( 'NONE', #7338, #19615 ) ;
#24075=DIRECTION ( 'NONE',  ( 0.000000000000000000, -0.2817325568414365544, 0.9594929736144953702 ) ) ;
#24077=EDGE_CURVE ( 'NONE', #20652, #8837, #1072, .T. ) ;
#24087=DIRECTION ( 'NONE',  ( 0.000000000000000000, 0.000000000000000000, 1.000000000000000000 ) ) ;
#24135=COLOUR_RGB('Light Blue',0.38,0.62,0.78);
#24136=FILL_AREA_STYLE_COLOUR('',#24135);
#24137=FILL_AREA_STYLE('',(#24136));
#24138=SURFACE_STYLE_FILL_AREA(#24137);
#24139=SURFACE_SIDE_STYLE('',(#24138));
#24140=SURFACE_STYLE_USAGE(.BOTH.,#24139);
#24141=PRESENTATION_STYLE_ASSIGNMENT((#24140));
ENDSEC;
END-ISO-10303-21;
